ISO-10303-21;
HEADER;
/* Generated by software containing ST-Developer
 * from STEP Tools, Inc. (www.steptools.com) 
 */

FILE_DESCRIPTION(
/* description */ (
'Independent welded steel electronics enclosure with removable sealed 
lid, internal mounting tray and two threaded cable entries. 300 x 220 
mm body. No ingress or electrical safety rating assigned.'),
/* implementation_level */ '2;1');

FILE_NAME(
/* name */ 'Entry locknut.step',
/* time_stamp */ '2026-11-14T09:13:27-08:00',
/* author */ (''),
/* organization */ (''),
/* preprocessor_version */ 'ST-DEVELOPER v20.2',
/* originating_system */ 'Autodesk Translation Framework v15.17.0.0',
/* authorisation */ '');

FILE_SCHEMA (('AUTOMOTIVE_DESIGN { 1 0 10303 214 3 1 1 }'));
ENDSEC;

DATA;
#10=MECHANICAL_DESIGN_GEOMETRIC_PRESENTATION_REPRESENTATION('',(#979),#94412);
#168=B_SPLINE_SURFACE_WITH_KNOTS('',3,3,((#93399,#93400,#93401,#93402,#93403,
#93404,#93405,#93406,#93407,#93408,#93409,#93410,#93411,#93412,#93413,#93414,
#93415,#93416,#93417,#93418,#93419,#93420,#93421,#93422,#93423,#93424,#93425,
#93426,#93427,#93428,#93429,#93430,#93431,#93432,#93433,#93434,#93435,#93436,
#93437,#93438,#93439,#93440,#93441,#93442,#93443,#93444,#93445,#93446,#93447,
#93448,#93449,#93450,#93451,#93452,#93453,#93454,#93455,#93456,#93457),
(#93458,#93459,#93460,#93461,#93462,#93463,#93464,#93465,#93466,#93467,
#93468,#93469,#93470,#93471,#93472,#93473,#93474,#93475,#93476,#93477,#93478,
#93479,#93480,#93481,#93482,#93483,#93484,#93485,#93486,#93487,#93488,#93489,
#93490,#93491,#93492,#93493,#93494,#93495,#93496,#93497,#93498,#93499,#93500,
#93501,#93502,#93503,#93504,#93505,#93506,#93507,#93508,#93509,#93510,#93511,
#93512,#93513,#93514,#93515,#93516),(#93517,#93518,#93519,#93520,#93521,
#93522,#93523,#93524,#93525,#93526,#93527,#93528,#93529,#93530,#93531,#93532,
#93533,#93534,#93535,#93536,#93537,#93538,#93539,#93540,#93541,#93542,#93543,
#93544,#93545,#93546,#93547,#93548,#93549,#93550,#93551,#93552,#93553,#93554,
#93555,#93556,#93557,#93558,#93559,#93560,#93561,#93562,#93563,#93564,#93565,
#93566,#93567,#93568,#93569,#93570,#93571,#93572,#93573,#93574,#93575),
(#93576,#93577,#93578,#93579,#93580,#93581,#93582,#93583,#93584,#93585,
#93586,#93587,#93588,#93589,#93590,#93591,#93592,#93593,#93594,#93595,#93596,
#93597,#93598,#93599,#93600,#93601,#93602,#93603,#93604,#93605,#93606,#93607,
#93608,#93609,#93610,#93611,#93612,#93613,#93614,#93615,#93616,#93617,#93618,
#93619,#93620,#93621,#93622,#93623,#93624,#93625,#93626,#93627,#93628,#93629,
#93630,#93631,#93632,#93633,#93634)),.UNSPECIFIED.,.F.,.F.,.F.,(4,4),(4,
1,1,1,1,1,1,1,1,1,1,1,1,1,1,1,1,1,1,1,1,1,1,1,1,1,1,1,1,1,1,1,1,1,1,1,1,
1,1,1,1,1,1,1,1,1,1,1,1,1,1,1,1,1,1,1,4),(-0.000103475830100935,0.0645568430532792),
(11.8498163896566,12.3348976354611,12.8198754054355,13.3048531754099,13.7898309453844,
14.2748087153588,14.7597864853332,15.2447642553077,15.7297420252821,16.2147197952565,
16.6996975652309,17.1846753352054,17.6696531051798,18.1546308751542,18.6396086451287,
19.1245864151031,19.6095641850775,20.0945419550519,20.5795197250264,21.0644974950008,
21.5494752649752,22.0344530349496,22.5194308049241,23.0044085748985,23.4893863448729,
23.9743641148474,24.4593418848218,24.9443196547962,25.4292974247706,25.9142751947451,
26.3992529647195,26.8842307346939,27.3692085046684,27.8541862746428,28.3391640446172,
28.8241418145916,29.3091195845661,29.7940973545405,30.2790751245149,30.7640528944893,
31.2490306644638,31.7340084344382,32.2189862044126,32.7039639743871,33.1889417443615,
33.6739195143359,34.1588972843103,34.6438750542848,35.1288528242592,35.6138305942336,
36.0988083642081,36.5837861341825,37.0687639041569,37.5537416741313,38.0387194441058,
38.5236972140802,39.0086749840546),.UNSPECIFIED.);
#169=B_SPLINE_SURFACE_WITH_KNOTS('',3,3,((#93865,#93866,#93867,#93868,#93869,
#93870,#93871,#93872,#93873,#93874,#93875,#93876,#93877,#93878,#93879,#93880,
#93881,#93882,#93883,#93884,#93885,#93886,#93887,#93888,#93889,#93890,#93891,
#93892,#93893,#93894,#93895,#93896,#93897,#93898,#93899,#93900,#93901,#93902,
#93903,#93904,#93905,#93906,#93907,#93908,#93909,#93910,#93911,#93912,#93913,
#93914,#93915,#93916,#93917,#93918,#93919,#93920,#93921,#93922,#93923),
(#93924,#93925,#93926,#93927,#93928,#93929,#93930,#93931,#93932,#93933,
#93934,#93935,#93936,#93937,#93938,#93939,#93940,#93941,#93942,#93943,#93944,
#93945,#93946,#93947,#93948,#93949,#93950,#93951,#93952,#93953,#93954,#93955,
#93956,#93957,#93958,#93959,#93960,#93961,#93962,#93963,#93964,#93965,#93966,
#93967,#93968,#93969,#93970,#93971,#93972,#93973,#93974,#93975,#93976,#93977,
#93978,#93979,#93980,#93981,#93982),(#93983,#93984,#93985,#93986,#93987,
#93988,#93989,#93990,#93991,#93992,#93993,#93994,#93995,#93996,#93997,#93998,
#93999,#94000,#94001,#94002,#94003,#94004,#94005,#94006,#94007,#94008,#94009,
#94010,#94011,#94012,#94013,#94014,#94015,#94016,#94017,#94018,#94019,#94020,
#94021,#94022,#94023,#94024,#94025,#94026,#94027,#94028,#94029,#94030,#94031,
#94032,#94033,#94034,#94035,#94036,#94037,#94038,#94039,#94040,#94041),
(#94042,#94043,#94044,#94045,#94046,#94047,#94048,#94049,#94050,#94051,
#94052,#94053,#94054,#94055,#94056,#94057,#94058,#94059,#94060,#94061,#94062,
#94063,#94064,#94065,#94066,#94067,#94068,#94069,#94070,#94071,#94072,#94073,
#94074,#94075,#94076,#94077,#94078,#94079,#94080,#94081,#94082,#94083,#94084,
#94085,#94086,#94087,#94088,#94089,#94090,#94091,#94092,#94093,#94094,#94095,
#94096,#94097,#94098,#94099,#94100)),.UNSPECIFIED.,.F.,.F.,.F.,(4,4),(4,
1,1,1,1,1,1,1,1,1,1,1,1,1,1,1,1,1,1,1,1,1,1,1,1,1,1,1,1,1,1,1,1,1,1,1,1,
1,1,1,1,1,1,1,1,1,1,1,1,1,1,1,1,1,1,1,4),(-6.74208202416338E-5,0.0645935329637062),
(14.3984001269719,14.8833778969463,15.3683556669207,15.8533334368951,16.3383112068696,
16.823288976844,17.3082667468184,17.7932445167929,18.2782222867673,18.7632000567417,
19.2481778267161,19.7331555966906,20.218133366665,20.7031111366394,21.1880889066139,
21.6730666765883,22.1580444465627,22.6430222165371,23.1279999865116,23.612977756486,
24.0979555264604,24.5829332964348,25.0679110664093,25.5528888363837,26.0378666063581,
26.5228443763326,27.007822146307,27.4927999162814,27.9777776862558,28.4627554562303,
28.9477332262047,29.4327109961791,29.9176887661536,30.402666536128,30.8876443061024,
31.3726220760768,31.8575998460513,32.3425776160257,32.8275553860001,33.3125331559745,
33.797510925949,34.2824886959234,34.7674664658978,35.2524442358723,35.7374220058467,
36.2223997758211,36.7073775457955,37.19235531577,37.6773330857444,38.1623108557188,
38.6472886256933,39.1322663956677,39.6172441656421,40.1022219356165,40.587199705591,
41.0721774755654,41.557258753435),.UNSPECIFIED.);
#903=B_SPLINE_CURVE_WITH_KNOTS('',3,(#91553,#91554,#91555,#91556,#91557,
#91558,#91559,#91560),.UNSPECIFIED.,.F.,.F.,(4,1,1,1,1,4),(36.7831101328767,
37.0687639041569,37.5537416741313,38.0387194441058,38.5236972140802,39.0086749840546),
 .UNSPECIFIED.);
#904=B_SPLINE_CURVE_WITH_KNOTS('',3,(#91563,#91564,#91565,#91566,#91567,
#91568,#91569,#91570,#91571),.UNSPECIFIED.,.F.,.F.,(4,1,1,1,1,1,4),(36.7831178657995,
37.19235531577,37.6773330857444,38.1623108557188,38.6472886256933,39.1322663956677,
39.5311215742981),.UNSPECIFIED.);
#905=B_SPLINE_CURVE_WITH_KNOTS('',3,(#91577,#91578,#91579,#91580,#91581,
#91582,#91583,#91584,#91585,#91586,#91587,#91588,#91589,#91590,#91591,#91592,
#91593,#91594,#91595,#91596,#91597,#91598,#91599,#91600,#91601,#91602,#91603,
#91604,#91605,#91606,#91607,#91608,#91609,#91610,#91611,#91612,#91613,#91614,
#91615,#91616,#91617,#91618,#91619,#91620,#91621,#91622,#91623,#91624,#91625,
#91626,#91627,#91628,#91629,#91630,#91631,#91632,#91633,#91634,#91635,#91636,
#91637,#91638,#91639,#91640,#91641,#91642,#91643,#91644,#91645,#91646,#91647,
#91648,#91649,#91650,#91651,#91652,#91653,#91654,#91655,#91656,#91657,#91658,
#91659,#91660,#91661,#91662,#91663,#91664,#91665,#91666,#91667,#91668,#91669,
#91670,#91671,#91672,#91673,#91674,#91675,#91676,#91677,#91678,#91679,#91680,
#91681,#91682,#91683,#91684,#91685,#91686,#91687,#91688,#91689,#91690,#91691,
#91692,#91693,#91694,#91695,#91696,#91697,#91698,#91699,#91700,#91701,#91702,
#91703,#91704,#91705,#91706,#91707,#91708,#91709,#91710,#91711,#91712,#91713,
#91714,#91715,#91716,#91717,#91718,#91719,#91720,#91721,#91722,#91723,#91724,
#91725,#91726,#91727,#91728,#91729,#91730,#91731,#91732,#91733,#91734,#91735,
#91736,#91737,#91738,#91739,#91740,#91741,#91742,#91743,#91744,#91745,#91746,
#91747,#91748,#91749,#91750,#91751,#91752,#91753,#91754),.UNSPECIFIED.,
 .F.,.F.,(4,3,3,3,3,3,3,3,3,3,3,3,3,3,3,3,3,3,3,3,3,3,3,3,3,3,3,3,3,3,3,
3,3,3,3,3,3,3,3,3,3,3,3,3,3,3,3,3,3,3,3,3,3,3,3,3,3,3,3,4),(30.4999165270005,
30.5734012599987,30.6468852042545,30.7203838367086,30.7640528944893,30.8375517166681,
30.9110384964528,30.9845177829552,31.0580025409672,31.1314864866202,31.2049851437445,
31.2490306644638,31.3225294639419,31.3960162209481,31.4694954846612,31.5429802200288,
31.6164641431568,31.6899627780857,31.7340084344382,31.8075072776668,31.8809940785443,
31.9544733861202,32.0279581650285,32.1014421314428,32.1749408089864,32.2189862044126,
32.2924849833025,32.3659717197231,32.4394509629135,32.5129356779971,32.5864195810097,
32.6599181962126,32.7039639743871,32.7774628074511,32.8509495979873,32.9244288950775,
32.9979136633574,33.0713976190805,33.1448962859055,33.1889417443615,33.2624406390856,
33.3359274919474,33.4094068518393,33.4828916831912,33.5563757020343,33.6298744316436,
33.6739195143359,33.7474179822581,33.8209044062208,33.8943833363914,33.9678677398215,
34.04135133247,34.1148496413041,34.1588972843103,34.2321178175882,34.3053253639141,
34.3785312054903,34.4517331639191,34.5249449085031,34.5575191894877),
 .UNSPECIFIED.);
#906=B_SPLINE_CURVE_WITH_KNOTS('',3,(#91755,#91756,#91757,#91758,#91759,
#91760,#91761,#91762,#91763),.UNSPECIFIED.,.F.,.F.,(4,1,1,1,1,1,4),(34.5575191894877,
34.6438750542848,35.1288528242592,35.6138305942336,36.0988083642081,36.5837861341825,
36.7831101328767),.UNSPECIFIED.);
#907=B_SPLINE_CURVE_WITH_KNOTS('',3,(#91765,#91766,#91767,#91768,#91769,
#91770,#91771,#91772,#91773),.UNSPECIFIED.,.F.,.F.,(4,1,1,1,1,1,4),(34.5575191894877,
34.7674664658978,35.2524442358723,35.7374220058467,36.2223997758211,36.7073775457955,
36.7831178657995),.UNSPECIFIED.);
#908=B_SPLINE_CURVE_WITH_KNOTS('',3,(#91774,#91775,#91776,#91777,#91778,
#91779,#91780,#91781,#91782,#91783,#91784,#91785),.UNSPECIFIED.,.F.,.F.,
(4,1,1,1,1,1,1,1,1,4),(30.4999349764196,30.8876443061024,31.3726220760768,
31.8575998460513,32.3425776160257,32.8275553860001,33.3125331559745,33.797510925949,
34.2824886959234,34.5575191894877),.UNSPECIFIED.);
#909=B_SPLINE_CURVE_WITH_KNOTS('',3,(#91791,#91792,#91793,#91794,#91795,
#91796,#91797,#91798,#91799,#91800,#91801,#91802),.UNSPECIFIED.,.F.,.F.,
(4,1,1,1,1,1,1,1,1,4),(24.2167278608201,24.4593418848218,24.9443196547962,
25.4292974247706,25.9142751947451,26.3992529647195,26.8842307346939,27.3692085046684,
27.8541862746428,28.2743338538108),.UNSPECIFIED.);
#910=B_SPLINE_CURVE_WITH_KNOTS('',3,(#91803,#91804,#91805,#91806,#91807,
#91808,#91809,#91810,#91811,#91812,#91813,#91814,#91815,#91816,#91817,#91818,
#91819,#91820,#91821,#91822,#91823,#91824,#91825,#91826,#91827,#91828,#91829,
#91830,#91831,#91832,#91833,#91834,#91835,#91836,#91837,#91838,#91839,#91840,
#91841,#91842,#91843,#91844,#91845,#91846,#91847,#91848,#91849,#91850,#91851,
#91852,#91853,#91854,#91855,#91856,#91857,#91858,#91859,#91860,#91861,#91862,
#91863,#91864,#91865,#91866,#91867,#91868,#91869,#91870,#91871,#91872,#91873,
#91874,#91875,#91876,#91877,#91878,#91879,#91880,#91881,#91882,#91883,#91884,
#91885,#91886,#91887,#91888,#91889,#91890,#91891,#91892,#91893,#91894,#91895,
#91896,#91897,#91898,#91899),.UNSPECIFIED.,.F.,.F.,(4,3,3,3,3,3,3,3,3,3,
3,3,3,3,3,3,3,3,3,3,3,3,3,3,3,3,3,3,3,3,3,3,4),(28.2743338823081,28.3391640446172,
28.4126628601145,28.4861496331911,28.5596289129786,28.6331136643131,28.7065976033206,
28.780096253892,28.8241418145916,28.8976406294224,28.9711274018309,29.0446066809508,
29.118091431623,29.1915753699723,29.2650740198958,29.3091195845661,29.382618400207,
29.4561051734266,29.5295844533558,29.6030692048292,29.6765531439741,29.7500517946789,
29.7940973545405,29.86759616995,29.9410829429414,30.0145622226464,30.0880469739032,
30.1615309128359,30.2350295633372,30.2790751245149,30.3525735089709,30.4262450179857,
30.4999165270005),.UNSPECIFIED.);
#911=B_SPLINE_CURVE_WITH_KNOTS('',3,(#91901,#91902,#91903,#91904,#91905,
#91906,#91907,#91908,#91909),.UNSPECIFIED.,.F.,.F.,(4,1,1,1,1,1,4),(28.2743338823081,
28.4627554562303,28.9477332262047,29.4327109961791,29.9176887661536,30.402666536128,
30.4999349764196),.UNSPECIFIED.);
#912=B_SPLINE_CURVE_WITH_KNOTS('',3,(#91910,#91911,#91912,#91913,#91914,
#91915,#91916,#91917,#91918,#91919,#91920,#91921),.UNSPECIFIED.,.F.,.F.,
(4,1,1,1,1,1,1,1,1,4),(24.2167503458098,24.5829332964348,25.0679110664093,
25.5528888363837,26.0378666063581,26.5228443763326,27.007822146307,27.4927999162814,
27.9777776862558,28.2743338823081),.UNSPECIFIED.);
#913=B_SPLINE_CURVE_WITH_KNOTS('',3,(#91927,#91928,#91929,#91930,#91931,
#91932,#91933,#91934,#91935,#91936,#91937,#91938,#91939,#91940,#91941,#91942,
#91943,#91944,#91945,#91946,#91947,#91948,#91949,#91950,#91951,#91952,#91953,
#91954,#91955,#91956,#91957,#91958,#91959,#91960,#91961,#91962,#91963,#91964,
#91965,#91966,#91967,#91968,#91969,#91970,#91971,#91972,#91973,#91974,#91975,
#91976,#91977,#91978,#91979,#91980,#91981,#91982,#91983,#91984,#91985,#91986,
#91987,#91988,#91989,#91990,#91991,#91992,#91993,#91994,#91995,#91996,#91997,
#91998,#91999,#92000,#92001,#92002,#92003,#92004,#92005,#92006,#92007,#92008,
#92009,#92010,#92011,#92012,#92013,#92014,#92015,#92016,#92017,#92018,#92019,
#92020,#92021,#92022,#92023),.UNSPECIFIED.,.F.,.F.,(4,3,3,3,3,3,3,3,3,3,
3,3,3,3,3,3,3,3,3,3,3,3,3,3,3,3,3,3,3,3,3,3,4),(15.707963270772,15.7844208965149,
15.8533334368951,15.926784338244,16.0002226755263,16.0736531423664,16.1470888545948,
16.2205237063183,16.2939735101588,16.3383112068696,16.4118254124913,16.4853277239607,
16.5588226436237,16.6323230769943,16.7058226958758,16.7793369216993,16.823288976844,
16.8967862501396,16.9702714821782,17.0437492266874,17.1172324624461,17.1907148995946,
17.2642120793322,17.3082667468184,17.3817630095345,17.455247191035,17.5287238482588,
17.6022059487071,17.6756872251217,17.7491832120583,17.7932445167929,17.8667471690964,
17.9335555972082),.UNSPECIFIED.);
#914=B_SPLINE_CURVE_WITH_KNOTS('',3,(#92025,#92026,#92027,#92028,#92029,
#92030),.UNSPECIFIED.,.F.,.F.,(4,1,1,4),(14.3984001269719,14.8833778969463,
15.3683556669207,15.707963267949),.UNSPECIFIED.);
#915=B_SPLINE_CURVE_WITH_KNOTS('',3,(#92034,#92035,#92036,#92037,#92038,
#92039,#92040),.UNSPECIFIED.,.F.,.F.,(4,1,1,1,4),(13.8759337553363,14.2748087153588,
14.7597864853332,15.2447642553077,15.707963267949),.UNSPECIFIED.);
#916=B_SPLINE_CURVE_WITH_KNOTS('',3,(#92041,#92042,#92043,#92044,#92045,
#92046,#92047,#92048,#92049),.UNSPECIFIED.,.F.,.F.,(4,1,1,1,1,1,4),(15.707963267949,
15.7297420252821,16.2147197952565,16.6996975652309,17.1846753352054,17.6696531051798,
17.9335366650258),.UNSPECIFIED.);
#917=B_SPLINE_CURVE_WITH_KNOTS('',3,(#92055,#92056,#92057,#92058,#92059,
#92060,#92061,#92062,#92063,#92064,#92065,#92066,#92067,#92068,#92069,#92070,
#92071,#92072,#92073,#92074,#92075,#92076,#92077,#92078,#92079,#92080,#92081,
#92082,#92083,#92084,#92085),.UNSPECIFIED.,.F.,.F.,(4,3,3,3,3,3,3,3,3,3,
4),(26.4423043696954,26.5177281543605,26.595752751477,26.6737773485935,
26.7487609216721,26.8237315844015,26.8986926879938,26.9736532318385,27.0486088408042,
27.1235698163438,27.158755118568),.UNSPECIFIED.);
#918=B_SPLINE_CURVE_WITH_KNOTS('',3,(#92088,#92089,#92090,#92091,#92092,
#92093,#92094,#92095,#92096,#92097,#92098,#92099,#92100,#92101,#92102,#92103,
#92104,#92105,#92106,#92107,#92108,#92109,#92110,#92111,#92112,#92113,#92114,
#92115,#92116,#92117,#92118,#92119,#92120,#92121,#92122,#92123,#92124,#92125,
#92126,#92127,#92128,#92129,#92130,#92131,#92132,#92133,#92134,#92135,#92136,
#92137,#92138,#92139,#92140,#92141,#92142,#92143,#92144,#92145,#92146,#92147,
#92148,#92149,#92150,#92151,#92152,#92153,#92154,#92155,#92156,#92157,#92158,
#92159,#92160,#92161,#92162,#92163,#92164,#92165,#92166,#92167,#92168,#92169,
#92170,#92171,#92172,#92173,#92174,#92175,#92176,#92177,#92178,#92179,#92180,
#92181,#92182,#92183,#92184,#92185,#92186,#92187,#92188,#92189,#92190,#92191,
#92192,#92193,#92194,#92195,#92196),.UNSPECIFIED.,.F.,.F.,(4,3,3,3,3,3,
3,3,3,3,3,3,3,3,3,3,3,3,3,3,3,3,3,3,3,3,3,3,3,3,3,3,3,3,3,3,4),(-25.1327214822589,
-25.0584480753609,-24.9841839577683,-24.9099156896555,-24.8356478285455,
-24.7613652784986,-24.7338662686958,-24.6593137477544,-24.584773583022,
-24.5102410217215,-24.4357028715999,-24.3611653050792,-24.2866130834149,
-24.2488884987214,-24.1743369699811,-24.0997978383104,-24.0252663476834,
-23.9507293171368,-23.8761928963057,-23.8016418528938,-23.763910728747,
-23.6893538742066,-23.6148093411984,-23.5402723904301,-23.4657298505343,
-23.3911879016937,-23.3166313367843,-23.2789329587725,-23.2043806207413,
-23.1298406614389,-23.055308327415,-22.9807704358101,-22.9062331452823,
-22.8316812245033,-22.7939551887981,-22.7146359699226,-22.7075993240011),
 .UNSPECIFIED.);
#919=B_SPLINE_CURVE_WITH_KNOTS('',3,(#92201,#92202,#92203,#92204,#92205,
#92206,#92207,#92208,#92209,#92210,#92211,#92212,#92213,#92214,#92215,#92216,
#92217),.UNSPECIFIED.,.F.,.F.,(4,1,1,1,1,1,1,1,1,1,1,1,1,1,4),(20.1591190804798,
20.369066338926,20.8540441089004,21.3390218788748,21.8239996488493,22.3089774188237,
22.7939551887981,23.2789329587725,23.763910728747,24.2488884987214,24.7338662686958,
25.2188440386703,25.7038218086447,26.1887995786191,26.4423043696954),
 .UNSPECIFIED.);
#920=B_SPLINE_CURVE_WITH_KNOTS('',3,(#92218,#92219,#92220,#92221,#92222,
#92223,#92224,#92225,#92226,#92227,#92228,#92229,#92230,#92231,#92232,#92233,
#92234),.UNSPECIFIED.,.F.,.F.,(4,1,1,1,1,1,1,1,1,1,1,1,1,1,4),(-22.7075993038896,
-22.3089774188237,-21.8239996488493,-21.3390218788748,-20.8540441089004,
-20.369066338926,-19.8840885689515,-19.3991107989771,-18.9141330290027,
-18.4291552590283,-17.9441774890538,-17.4591997190794,-16.974221949105,
-16.4892441791305,-16.4244140168215),.UNSPECIFIED.);
#921=B_SPLINE_CURVE_WITH_KNOTS('',3,(#92239,#92240,#92241,#92242,#92243,
#92244,#92245,#92246,#92247,#92248,#92249,#92250,#92251,#92252,#92253,#92254,
#92255,#92256,#92257,#92258,#92259,#92260,#92261,#92262,#92263,#92264,#92265,
#92266,#92267,#92268,#92269,#92270,#92271,#92272,#92273,#92274,#92275,#92276,
#92277,#92278,#92279,#92280,#92281,#92282,#92283,#92284,#92285,#92286,#92287,
#92288,#92289,#92290,#92291,#92292,#92293,#92294,#92295,#92296,#92297,#92298,
#92299,#92300,#92301,#92302,#92303,#92304,#92305,#92306,#92307,#92308,#92309,
#92310,#92311,#92312,#92313,#92314,#92315,#92316,#92317,#92318,#92319,#92320,
#92321,#92322,#92323,#92324,#92325,#92326,#92327,#92328,#92329,#92330,#92331,
#92332,#92333,#92334,#92335,#92336,#92337,#92338,#92339,#92340,#92341,#92342,
#92343,#92344,#92345,#92346,#92347,#92348,#92349,#92350,#92351,#92352,#92353,
#92354,#92355,#92356,#92357,#92358,#92359,#92360,#92361,#92362,#92363,#92364,
#92365,#92366,#92367,#92368,#92369,#92370,#92371,#92372,#92373,#92374,#92375,
#92376,#92377,#92378,#92379,#92380,#92381,#92382,#92383,#92384,#92385,#92386,
#92387,#92388,#92389,#92390,#92391,#92392,#92393,#92394,#92395,#92396,#92397,
#92398,#92399,#92400,#92401,#92402,#92403,#92404,#92405,#92406,#92407,#92408,
#92409,#92410,#92411,#92412,#92413,#92414,#92415,#92416,#92417,#92418,#92419,
#92420,#92421,#92422,#92423,#92424,#92425,#92426,#92427,#92428,#92429,#92430,
#92431,#92432,#92433,#92434,#92435,#92436,#92437,#92438,#92439,#92440,#92441,
#92442,#92443,#92444,#92445,#92446,#92447,#92448,#92449,#92450,#92451,#92452,
#92453,#92454,#92455,#92456,#92457,#92458,#92459,#92460,#92461,#92462,#92463,
#92464,#92465,#92466,#92467,#92468,#92469,#92470,#92471,#92472,#92473,#92474,
#92475,#92476,#92477,#92478,#92479,#92480,#92481,#92482,#92483,#92484,#92485,
#92486,#92487,#92488,#92489,#92490,#92491,#92492,#92493,#92494,#92495,#92496,
#92497,#92498,#92499,#92500,#92501,#92502,#92503,#92504,#92505,#92506,#92507,
#92508,#92509,#92510,#92511,#92512),.UNSPECIFIED.,.F.,.F.,(4,3,3,3,3,3,
3,3,3,3,3,3,3,3,3,3,3,3,3,3,3,3,3,3,3,3,3,3,3,3,3,3,3,3,3,3,3,3,3,3,3,3,
3,3,3,3,3,3,3,3,3,3,3,3,3,3,3,3,3,3,3,3,3,3,3,3,3,3,3,3,3,3,3,3,3,3,3,3,
3,3,3,3,3,3,3,3,3,3,3,3,3,4),(13.875933755441,13.9523182994839,14.0287249568119,
14.0643553292584,14.1389094507212,14.2134512150667,14.2879853701618,14.3625250938589,
14.4370642196202,14.5116179688183,14.5493330992328,14.6238872206886,14.6984289850271,
14.7729631401157,14.847502863806,14.9220419895609,14.9965957387525,15.0343108692073,
15.1088649906549,15.1834067549852,15.2579409100652,15.3324806337471,15.4070197594934,
15.4815735086768,15.5192886391817,15.5938427606885,15.6683845250781,15.7429186802175,
15.8174584039587,15.8919975297641,15.9665512790057,16.0042664091561,16.0788205304861,
16.1533622946982,16.2278964496601,16.3024361732247,16.3769752988544,16.4515290479228,
16.4892441791306,16.5637983008486,16.63834006545,16.7128742208012,16.7874139447523,
16.8619530707664,16.9365068202134,16.974221949105,17.0487760701572,17.1233178340913,
17.1978519887755,17.2723917120651,17.3469308374218,17.421484586222,17.4591997190794,
17.5337538409431,17.6082956056894,17.6828297611844,17.7573694852764,17.8319086114295,
17.9064623610119,17.9441774890538,18.0187316106808,18.0932733751937,18.1678075304591,
18.2423472543295,18.3168863802656,18.3914401296395,18.4291552590283,18.5037093783136,
18.5782511404699,18.652785293371,18.7273250148823,18.8018641384667,18.8764178855145,
18.9141330290027,18.9886871574017,19.0632289287109,19.1377630907763,19.2123028214034,
19.2868419540601,19.361395710057,19.3991107989771,19.4736649046515,19.5482066531576,
19.6227407924106,19.6972805003736,19.7718196104903,19.8463733442772,19.8840885689515,
19.9590919762986,20.0340811182084,20.1090627868793,20.1591190625159),
 .UNSPECIFIED.);
#922=B_SPLINE_CURVE_WITH_KNOTS('',3,(#92513,#92514,#92515,#92516,#92517,
#92518,#92519,#92520,#92521,#92522,#92523,#92524,#92525,#92526,#92527,#92528,
#92529,#92530,#92531,#92532,#92533,#92534,#92535,#92536,#92537,#92538,#92539,
#92540,#92541,#92542,#92543,#92544,#92545,#92546,#92547,#92548,#92549,#92550,
#92551,#92552,#92553,#92554,#92555,#92556,#92557,#92558,#92559,#92560,#92561,
#92562,#92563,#92564,#92565,#92566,#92567,#92568,#92569,#92570,#92571,#92572,
#92573,#92574,#92575,#92576,#92577,#92578,#92579,#92580,#92581,#92582,#92583,
#92584,#92585,#92586,#92587,#92588,#92589,#92590,#92591,#92592,#92593,#92594,
#92595,#92596,#92597,#92598,#92599,#92600,#92601,#92602,#92603,#92604,#92605,
#92606,#92607,#92608,#92609,#92610,#92611,#92612,#92613,#92614,#92615,#92616,
#92617,#92618,#92619,#92620,#92621,#92622,#92623,#92624,#92625,#92626,#92627,
#92628,#92629,#92630,#92631,#92632,#92633,#92634,#92635,#92636,#92637,#92638,
#92639,#92640,#92641,#92642,#92643,#92644,#92645,#92646),.UNSPECIFIED.,
 .F.,.F.,(4,2,2,2,2,2,2,2,2,2,2,2,2,2,2,2,2,2,2,2,2,2,2,2,2,2,2,2,2,2,2,
2,2,2,2,2,2,2,2,2,2,2,2,2,2,2,2,2,2,2,2,2,2,2,2,2,2,2,2,2,2,2,2,2,2,2,4),
(-11.9638822364953,-11.8246083790295,-11.7850044251456,-11.6666270333911,
-11.5743370158719,-11.5215522030845,-11.4158180763237,-11.3232843333124,
-11.2057648180386,-11.1128389478311,-11.0601758544271,-10.9543628118302,
-10.8617403001231,-10.7431358111963,-10.6510075779731,-10.5981889032602,
-10.4924721527717,-10.3999587256611,-10.2827338271333,-10.1895841942765,
-10.1369613809018,-10.0311187869314,-9.93846355365529,-9.81949932331109,
-9.72762965184425,-9.67475748844462,-9.56907034488649,-9.47659094888344,
-9.35985373725229,-9.26633560082532,-9.21377938322884,-9.10789030268266,
-9.01518304757671,-8.89564575967799,-8.80418932594369,-8.75123141475238,
-8.64559381869177,-8.553170722345,-8.43726518248948,-8.34311795190573,-8.29067395121869,
-8.18470869086248,-8.09191538508498,-7.97144842696542,-7.88066151373026,
-7.82756201475512,-7.72200805187734,-7.62967907343574,-7.51531308141315,
-7.4216169743245,-7.37052605180074,-7.26053897090964,-7.16810461835174,
-7.05208466657828,-6.95801620826587,-6.90555528047204,-6.79959525914511,
-6.70680909004534,-6.58645618078307,-6.49557951578119,-6.44249606341095,
-6.33692658741559,-6.24458135416368,-6.12999569275972,-6.03483388751013,
-5.98256195553799,-5.98255038595961),.UNSPECIFIED.);
#923=B_SPLINE_CURVE_WITH_KNOTS('',3,(#92652,#92653,#92654,#92655,#92656,
#92657,#92658,#92659,#92660,#92661,#92662,#92663,#92664,#92665,#92666,#92667,
#92668,#92669,#92670,#92671,#92672,#92673,#92674,#92675,#92676,#92677,#92678,
#92679,#92680,#92681,#92682,#92683,#92684,#92685,#92686,#92687,#92688,#92689,
#92690,#92691,#92692,#92693,#92694,#92695,#92696,#92697,#92698,#92699,#92700,
#92701,#92702,#92703,#92704,#92705,#92706,#92707,#92708,#92709,#92710,#92711,
#92712,#92713,#92714,#92715,#92716,#92717,#92718,#92719,#92720,#92721,#92722,
#92723,#92724,#92725,#92726,#92727,#92728,#92729,#92730,#92731,#92732,#92733,
#92734,#92735,#92736,#92737,#92738,#92739,#92740,#92741,#92742,#92743,#92744,
#92745,#92746,#92747,#92748,#92749,#92750,#92751,#92752,#92753,#92754,#92755,
#92756,#92757,#92758,#92759,#92760,#92761,#92762,#92763,#92764,#92765,#92766,
#92767,#92768,#92769,#92770,#92771,#92772,#92773,#92774,#92775,#92776,#92777,
#92778,#92779,#92780,#92781,#92782,#92783,#92784,#92785,#92786,#92787,#92788,
#92789,#92790,#92791,#92792,#92793,#92794,#92795,#92796,#92797,#92798,#92799,
#92800,#92801,#92802,#92803,#92804,#92805,#92806,#92807,#92808,#92809,#92810,
#92811,#92812,#92813,#92814,#92815,#92816,#92817,#92818,#92819,#92820),
 .UNSPECIFIED.,.F.,.F.,(4,3,3,3,3,3,3,3,3,3,3,3,3,3,3,3,3,3,3,3,3,3,3,3,
3,3,3,3,3,3,3,3,3,3,3,3,3,3,3,3,3,3,3,3,3,3,3,3,3,3,3,3,3,3,3,3,4),(-3.85804340235828,
-3.78362003001371,-3.70920911636523,-3.63480552147699,-3.56039643756462,
-3.48598674990222,-3.41156317849099,-3.394844389821,-3.32029297434401,-3.24575391528527,
-3.17122245665661,-3.09668539716685,-3.02214891259346,-2.94759775312034,
-2.90986661984657,-2.83531402775715,-2.76077381741281,-2.68624123601308,
-2.61170310407322,-2.53716557759435,-2.46261342883627,-2.42488884987214,
-2.35031879820004,-2.27576102010989,-2.2012108168873,-2.12665510830727,
-2.05210006164846,-1.97753058928639,-1.93991107989771,-1.86540678926133,
-1.79091504818262,-1.71643095751296,-1.64194100546716,-1.56745139902857,
-1.49294647488379,-1.45493330992328,-1.38026437631378,-1.30560745184444,
-1.23095814532789,-1.15630411372744,-1.08165136647512,-1.00698575704174,
-0.969955539948856,-0.895616091376641,-0.821289274965453,-0.746969710952536,
-0.672642549632695,-0.598314479491087,-0.523968178294443,-0.484977769974428,
-0.409993929498993,-0.335022998273941,-0.260061626001027,-0.185100815258932,
-0.110144940981982,-0.0351837042315546,-1.28400083291566E-15),
 .UNSPECIFIED.);
#924=B_SPLINE_CURVE_WITH_KNOTS('',3,(#92823,#92824,#92825,#92826,#92827,
#92828,#92829,#92830,#92831,#92832,#92833,#92834,#92835,#92836,#92837,#92838,
#92839,#92840,#92841,#92842,#92843,#92844,#92845,#92846,#92847,#92848,#92849,
#92850,#92851,#92852,#92853,#92854,#92855,#92856,#92857,#92858,#92859,#92860,
#92861,#92862,#92863,#92864,#92865,#92866,#92867,#92868,#92869,#92870,#92871,
#92872,#92873,#92874,#92875,#92876,#92877,#92878,#92879,#92880,#92881,#92882,
#92883,#92884,#92885,#92886,#92887,#92888,#92889,#92890,#92891,#92892,#92893,
#92894,#92895,#92896,#92897,#92898,#92899,#92900,#92901,#92902,#92903,#92904,
#92905,#92906,#92907,#92908,#92909,#92910,#92911,#92912,#92913,#92914,#92915,
#92916,#92917,#92918,#92919,#92920,#92921,#92922,#92923,#92924,#92925,#92926,
#92927,#92928,#92929,#92930,#92931,#92932,#92933,#92934,#92935,#92936),
 .UNSPECIFIED.,.F.,.F.,(4,2,2,2,2,2,2,2,2,2,2,2,2,2,2,2,2,2,2,2,2,2,2,2,
2,2,2,2,2,2,2,2,2,2,2,2,2,2,2,2,2,2,2,2,2,2,2,2,2,2,2,2,2,2,2,2,4),(-11.2826168307778,
-11.1762469541903,-11.125251757876,-11.0024781283703,-10.913262956463,-10.8603484703286,
-10.7551997075349,-10.6630450538886,-10.5459538031153,-10.4526792588227,
-10.4002938827596,-10.2941831409333,-10.2013817166273,-10.0822414864162,
-9.99048362981615,-9.93747996123894,-9.83187816625984,-9.73943941398009,
-9.6233884934606,-9.52931042843913,-9.4768674967077,-9.37088092946969,-9.2780814777363,
-9.15745351747334,-9.06676588322009,-9.01363578521839,-8.90807491228135,
-8.86523714088575,-8.7827607709068,-8.65107318309677,-8.59051603867521,
-8.49516414937743,-8.3776343569781,-8.28788852307351,-8.18483687985127,
-8.12709756418481,-8.01873894340126,-7.9048736756614,-7.738383419085,-7.68875444778559,
-7.63979152259541,-7.5167676520058,-7.47512511439043,-7.39235876813903,
-7.26177739136488,-7.20372069393057,-7.09423898142508,-6.98111650500347,
-6.81154393892334,-6.74566579468266,-6.64203139701929,-6.52111251348614,
-6.34946821939356,-6.28376743197177,-6.18037248448461,-6.05975907348889,
-5.98309645076391),.UNSPECIFIED.);
#925=B_SPLINE_CURVE_WITH_KNOTS('',3,(#92938,#92939,#92940,#92941,#92942,
#92943,#92944,#92945,#92946,#92947,#92948,#92949,#92950,#92951,#92952,#92953,
#92954,#92955,#92956,#92957,#92958,#92959,#92960,#92961,#92962,#92963,#92964,
#92965,#92966,#92967,#92968,#92969,#92970,#92971,#92972,#92973,#92974,#92975,
#92976,#92977,#92978,#92979,#92980,#92981,#92982,#92983,#92984,#92985,#92986,
#92987,#92988,#92989,#92990,#92991,#92992,#92993,#92994,#92995,#92996,#92997,
#92998,#92999,#93000,#93001,#93002,#93003,#93004,#93005,#93006,#93007,#93008,
#93009,#93010,#93011,#93012,#93013,#93014,#93015,#93016,#93017,#93018,#93019,
#93020,#93021,#93022,#93023,#93024,#93025,#93026,#93027,#93028,#93029,#93030,
#93031,#93032,#93033,#93034,#93035,#93036,#93037,#93038,#93039,#93040,#93041,
#93042,#93043,#93044,#93045,#93046,#93047,#93048,#93049,#93050,#93051,#93052,
#93053),.UNSPECIFIED.,.F.,.F.,(4,2,2,2,2,2,2,2,2,2,2,2,2,2,2,2,2,2,2,2,
2,2,2,2,2,2,2,2,2,2,2,2,2,2,2,2,2,2,2,2,2,2,2,2,2,2,2,2,2,2,2,2,2,2,2,2,
2,4),(-5.98309645076391,-5.96179369819221,-5.87096264149203,-5.8159836647812,
-5.7322865699612,-5.64206252030099,-5.55924398589808,-5.51771648526159,
-5.39571852179474,-5.34633766037634,-5.22017712755589,-5.12476205799574,
-5.00448193589412,-4.90358088052579,-4.83962638261926,-4.66429586956545,
-4.54360496937077,-4.44139652900391,-4.37654387058763,-4.20314070678402,
-4.08320416938816,-3.97905656025761,-3.9127972674704,-3.74229346245245,
-3.62029939866371,-3.51762452494512,-3.45244184022386,-3.27973147588721,
-3.15905809947262,-3.05558871364941,-2.98983174029597,-2.81830834359997,
-2.69742813409663,-2.59369687418265,-2.52774726666072,-2.35661682998401,
-2.23138451959968,-2.13347087231659,-2.07142227037775,-1.89177931761666,
-1.77501663505352,-1.67613549123449,-1.62112530578369,-1.53015943268023,
-1.43230303448501,-1.31210058664763,-1.20826608339593,-1.14224024437481,
-0.97125966403786,-0.847074837591189,-0.747627482567506,-0.684625096025565,
-0.507174670272276,-0.387108301925727,-0.285075944693684,-0.220346759625927,
-0.0744964973377189,-0.0001310575238002),.UNSPECIFIED.);
#926=B_SPLINE_CURVE_WITH_KNOTS('',3,(#93054,#93055,#93056,#93057,#93058,
#93059,#93060,#93061,#93062,#93063,#93064,#93065,#93066,#93067,#93068,#93069,
#93070,#93071,#93072,#93073,#93074,#93075,#93076,#93077,#93078,#93079,#93080,
#93081,#93082,#93083,#93084,#93085,#93086,#93087,#93088,#93089,#93090,#93091,
#93092,#93093,#93094,#93095,#93096,#93097,#93098,#93099,#93100,#93101,#93102,
#93103,#93104,#93105,#93106,#93107,#93108,#93109,#93110,#93111,#93112,#93113,
#93114,#93115,#93116,#93117,#93118,#93119,#93120,#93121,#93122,#93123,#93124,
#93125,#93126,#93127,#93128,#93129,#93130,#93131,#93132,#93133,#93134,#93135,
#93136,#93137,#93138,#93139,#93140,#93141,#93142,#93143,#93144,#93145,#93146,
#93147,#93148,#93149,#93150,#93151,#93152,#93153,#93154,#93155,#93156,#93157,
#93158,#93159,#93160,#93161,#93162,#93163,#93164,#93165,#93166,#93167,#93168,
#93169,#93170,#93171,#93172,#93173,#93174,#93175),.UNSPECIFIED.,.F.,.F.,
(4,2,2,2,2,2,2,2,2,2,2,2,2,2,2,2,2,2,2,2,2,2,2,2,2,2,2,2,2,2,2,2,2,2,2,
2,2,2,2,2,2,2,2,2,2,2,2,2,2,2,2,2,2,2,2,2,2,2,2,2,4),(-5.98255038595961,
-5.90311477667104,-5.80173701362555,-5.70830267876734,-5.60178531374225,
-5.55015212437345,-5.41169735934466,-5.32015103300485,-5.20817938309062,
-5.10826992870272,-5.05297087285603,-4.96075345802036,-4.86390438307122,
-4.74332112600621,-4.64111274998532,-4.5762623599312,-4.40286879072047,
-4.28277227534319,-4.17885092835326,-4.11276209785121,-3.94192825741033,
-3.81850957491799,-3.71795461265881,-3.65423326151255,-3.47840649608167,
-3.35992304227894,-3.26149860727525,-3.20661906968306,-3.11620539458233,
-3.01790489144965,-2.89723410425966,-2.79358318138824,-2.72769335289786,
-2.55815918652112,-2.4450887916942,-2.33554639484681,-2.27747578243195,
-2.14689175849319,-2.06413358293121,-2.02248679724396,-1.89940786726995,
-1.85047156732237,-1.71740925151478,-1.62591851574838,-1.51377348428522,
-1.41419276829883,-1.35899612404205,-1.26721981099963,-1.17002106870236,
-1.05004144920438,-0.94659983994607,-0.880841108726548,-0.709318050707547,
-0.580922441173507,-0.490518786270498,-0.435174627672907,-0.342764808991137,
-0.246067136066954,-0.170663750263522,-0.032663736953733,-0.000134629797728273),
 .UNSPECIFIED.);
#927=B_SPLINE_CURVE_WITH_KNOTS('',3,(#93178,#93179,#93180,#93181,#93182,
#93183,#93184,#93185,#93186,#93187,#93188,#93189),.UNSPECIFIED.,.F.,.F.,
(4,1,1,1,1,1,1,1,1,4),(17.9335366650258,18.1546308751542,18.6396086451287,
19.1245864151031,19.6095641850775,20.0945419550519,20.5795197250264,21.0644974950008,
21.5494752649752,21.9911485751285),.UNSPECIFIED.);
#928=B_SPLINE_CURVE_WITH_KNOTS('',3,(#93190,#93191,#93192,#93193,#93194,
#93195,#93196,#93197,#93198),.UNSPECIFIED.,.F.,.F.,(4,1,1,1,1,1,4),(21.9911485751285,
22.0344530349496,22.5194308049241,23.0044085748985,23.4893863448729,23.9743641148474,
24.2167278608201),.UNSPECIFIED.);
#929=B_SPLINE_CURVE_WITH_KNOTS('',3,(#93200,#93201,#93202,#93203,#93204,
#93205,#93206,#93207,#93208),.UNSPECIFIED.,.F.,.F.,(4,1,1,1,1,1,4),(21.9911486045731,
22.1580444465627,22.6430222165371,23.1279999865116,23.612977756486,24.0979555264604,
24.2167503458098),.UNSPECIFIED.);
#930=B_SPLINE_CURVE_WITH_KNOTS('',3,(#93209,#93210,#93211,#93212,#93213,
#93214,#93215,#93216,#93217,#93218,#93219,#93220,#93221,#93222,#93223,#93224,
#93225,#93226,#93227,#93228,#93229,#93230,#93231,#93232,#93233,#93234,#93235,
#93236,#93237,#93238,#93239,#93240,#93241,#93242,#93243,#93244,#93245,#93246,
#93247,#93248,#93249,#93250,#93251,#93252,#93253,#93254,#93255,#93256,#93257,
#93258,#93259,#93260,#93261,#93262,#93263,#93264,#93265,#93266,#93267,#93268,
#93269,#93270,#93271,#93272,#93273,#93274,#93275,#93276,#93277,#93278,#93279,
#93280,#93281,#93282,#93283,#93284,#93285,#93286,#93287,#93288,#93289,#93290,
#93291,#93292,#93293,#93294,#93295,#93296,#93297,#93298,#93299,#93300,#93301,
#93302,#93303,#93304,#93305,#93306,#93307,#93308,#93309,#93310,#93311,#93312,
#93313,#93314,#93315,#93316,#93317,#93318,#93319,#93320,#93321,#93322,#93323,
#93324,#93325,#93326,#93327,#93328,#93329,#93330,#93331,#93332,#93333,#93334,
#93335,#93336,#93337,#93338,#93339,#93340,#93341,#93342,#93343,#93344,#93345,
#93346,#93347,#93348,#93349,#93350,#93351,#93352,#93353,#93354,#93355,#93356,
#93357,#93358,#93359,#93360,#93361,#93362,#93363,#93364,#93365,#93366,#93367,
#93368,#93369,#93370,#93371,#93372,#93373,#93374,#93375,#93376,#93377,#93378,
#93379,#93380,#93381,#93382,#93383,#93384,#93385,#93386),.UNSPECIFIED.,
 .F.,.F.,(4,3,3,3,3,3,3,3,3,3,3,3,3,3,3,3,3,3,3,3,3,3,3,3,3,3,3,3,3,3,3,
3,3,3,3,3,3,3,3,3,3,3,3,3,3,3,3,3,3,3,3,3,3,3,3,3,3,3,3,4),(17.9335555972082,
18.007038108634,18.0805259216794,18.1540125117814,18.2275142346009,18.2782222867673,
18.3517193566403,18.4252043632004,18.498681860891,18.5721648191973,18.6456469619359,
18.7191438227812,18.7632000567417,18.836699748599,18.9101874079279,18.9836675811948,
19.0571532306,19.1306380687981,19.2041376145015,19.2481778267161,19.3216763040303,
19.395162735418,19.4686416710373,19.5421260768971,19.6156096702605,19.6891079771531,
19.7331555966906,19.8066544900448,19.8801413415835,19.9536207002029,20.0271055303679,
20.1005895480742,20.1740882766318,20.218133366665,20.291632198477,20.3651189882224,
20.4385982849825,20.5120830536293,20.5855670101137,20.659065678305,20.7031111366394,
20.7766099170402,20.8500966545468,20.9235758983977,20.9970606134957,21.0705445161567,
21.1440431304441,21.1880889066139,21.2615877487943,21.3350745488855,21.4085538559384,
21.4820386347234,21.5555226012415,21.629021279239,21.6730666765883,21.7466012061225,
21.8201249209659,21.893639208639,21.9671526510914,21.9911485751285),
 .UNSPECIFIED.);
#931=B_SPLINE_CURVE_WITH_KNOTS('',3,(#93635,#93636,#93637,#93638,#93639,
#93640,#93641,#93642,#93643,#93644,#93645,#93646,#93647,#93648,#93649,#93650,
#93651,#93652,#93653,#93654,#93655,#93656,#93657,#93658,#93659,#93660,#93661,
#93662,#93663,#93664,#93665,#93666,#93667,#93668,#93669,#93670,#93671,#93672,
#93673,#93674,#93675,#93676,#93677,#93678,#93679,#93680,#93681,#93682,#93683,
#93684,#93685,#93686,#93687,#93688,#93689,#93690,#93691,#93692,#93693,#93694,
#93695,#93696,#93697,#93698,#93699,#93700,#93701,#93702,#93703,#93704,#93705,
#93706,#93707,#93708,#93709,#93710,#93711,#93712,#93713,#93714,#93715,#93716,
#93717,#93718,#93719,#93720,#93721,#93722,#93723,#93724,#93725,#93726,#93727,
#93728,#93729,#93730,#93731,#93732,#93733,#93734,#93735,#93736,#93737,#93738,
#93739,#93740,#93741,#93742,#93743,#93744,#93745,#93746,#93747,#93748,#93749),
 .UNSPECIFIED.,.F.,.F.,(4,3,3,3,3,3,3,3,3,3,3,3,3,3,3,3,3,3,3,3,3,3,3,3,
3,3,3,3,3,3,3,3,3,3,3,3,3,3,4),(0.,0.0739126635462495,0.150740513686272,
0.225935951919889,0.303580008013115,0.381224064106341,0.389885207948467,
0.400073548669132,0.474555444274402,0.487104039232364,0.561377161816764,
0.635987840137627,0.710367183555496,0.774793244282009,0.786415201228137,
0.860297905292171,0.934077532582566,0.968071426461548,1.04206547690771,
1.1158601918424,1.15671189269083,1.16870781265367,1.24198330165962,1.31537204770392,
1.38812719592645,1.4426737986298,1.50108005437742,1.52663279126701,1.54012983179738,
1.55002299318499,1.57202511761386,1.6448077654029,1.71108678520487,1.76079605005635,
1.77610764545378,1.84829504017901,1.9099238446108,1.98235653582154,1.99217144768675),
 .UNSPECIFIED.);
#932=B_SPLINE_CURVE_WITH_KNOTS('',3,(#93750,#93751,#93752,#93753,#93754,
#93755,#93756,#93757,#93758,#93759,#93760,#93761,#93762,#93763,#93764,#93765,
#93766,#93767,#93768,#93769,#93770,#93771,#93772,#93773,#93774,#93775,#93776,
#93777,#93778,#93779,#93780,#93781,#93782,#93783,#93784,#93785,#93786,#93787,
#93788,#93789,#93790,#93791,#93792,#93793,#93794,#93795,#93796,#93797,#93798,
#93799,#93800,#93801,#93802,#93803,#93804,#93805,#93806,#93807,#93808,#93809,
#93810,#93811,#93812,#93813,#93814,#93815,#93816,#93817,#93818,#93819,#93820,
#93821,#93822,#93823,#93824,#93825,#93826,#93827,#93828,#93829,#93830,#93831,
#93832,#93833,#93834,#93835,#93836,#93837,#93838,#93839,#93840,#93841,#93842,
#93843,#93844,#93845,#93846,#93847,#93848,#93849,#93850,#93851,#93852,#93853,
#93854,#93855,#93856,#93857,#93858,#93859,#93860,#93861,#93862,#93863,#93864),
 .UNSPECIFIED.,.F.,.F.,(4,3,3,3,3,3,3,3,3,3,3,3,3,3,3,3,3,3,3,3,3,3,3,3,
3,3,3,3,3,3,3,3,3,3,3,3,3,3,4),(0.,0.0709761209897443,0.142931446040141,
0.21545925542993,0.287856627714121,0.332469159572249,0.365928558465845,
0.375861814980538,0.448916300094163,0.466306755146632,0.538880173574122,
0.611947284117477,0.684979149532332,0.748511465508852,0.756781309220838,
0.830210843243463,0.903989318076003,0.939195971997139,1.01278289101164,
1.08650672760772,1.12800034646411,1.14013519160853,1.21408946536429,1.28844299347222,
1.36258786411151,1.41845567845884,1.47903742889201,1.50554194470653,1.51621439279437,
1.52551173241115,1.59979138412183,1.67562095857243,1.73249313941038,1.74983333918112,
1.76344979329115,1.83852338945091,1.90310968192423,1.97800052830964,1.98979055697635),
 .UNSPECIFIED.);
#933=B_SPLINE_CURVE_WITH_KNOTS('',3,(#94101,#94102,#94103,#94104,#94105,
#94106,#94107,#94108,#94109,#94110,#94111,#94112,#94113,#94114,#94115,#94116,
#94117,#94118,#94119,#94120,#94121,#94122,#94123,#94124,#94125,#94126,#94127,
#94128,#94129,#94130,#94131,#94132,#94133,#94134,#94135,#94136,#94137,#94138,
#94139,#94140,#94141,#94142,#94143,#94144,#94145,#94146,#94147,#94148,#94149,
#94150,#94151,#94152,#94153,#94154,#94155,#94156,#94157,#94158,#94159,#94160,
#94161,#94162,#94163,#94164,#94165,#94166,#94167,#94168,#94169,#94170,#94171,
#94172,#94173,#94174,#94175,#94176,#94177,#94178,#94179,#94180,#94181,#94182,
#94183,#94184,#94185,#94186,#94187,#94188,#94189,#94190,#94191,#94192,#94193,
#94194,#94195,#94196,#94197,#94198,#94199,#94200,#94201,#94202,#94203,#94204,
#94205,#94206,#94207,#94208,#94209,#94210,#94211,#94212),.UNSPECIFIED.,
 .F.,.F.,(4,3,3,3,3,3,3,3,3,3,3,3,3,3,3,3,3,3,3,3,3,3,3,3,3,3,3,3,3,3,3,
3,3,3,3,3,3,4),(0.,0.0707412612887614,0.144538066072586,0.217130768668796,
0.291529624546427,0.365928480424058,0.374378535179976,0.447428921852669,
0.466306755146633,0.538735411390327,0.611788295327192,0.684950044616232,
0.748511526461462,0.757906047956915,0.831343763816251,0.905121500651129,
0.939195971997151,1.01278287709315,1.08650671046459,1.12800033146387,1.14013518859003,
1.21408944402746,1.28844296470764,1.36258783663024,1.41845567845885,1.47903742889203,
1.50554194470654,1.51621439199532,1.52551173161284,1.5997913820326,1.67562095700551,
1.7324931382352,1.74983333999573,1.76344979518143,1.83852339153841,1.90310968192426,
1.97800053497444,1.98979104577926),.UNSPECIFIED.);
#934=B_SPLINE_CURVE_WITH_KNOTS('',3,(#94214,#94215,#94216,#94217),
 .UNSPECIFIED.,.F.,.F.,(4,4),(0.,0.000891519205898623),.UNSPECIFIED.);
#935=B_SPLINE_CURVE_WITH_KNOTS('',3,(#94218,#94219,#94220,#94221,#94222,
#94223,#94224,#94225,#94226,#94227,#94228,#94229,#94230,#94231,#94232,#94233,
#94234,#94235,#94236,#94237,#94238,#94239,#94240,#94241,#94242,#94243,#94244,
#94245,#94246,#94247,#94248,#94249,#94250,#94251,#94252,#94253,#94254,#94255,
#94256,#94257,#94258,#94259,#94260,#94261,#94262,#94263,#94264,#94265,#94266,
#94267,#94268,#94269,#94270,#94271,#94272,#94273,#94274,#94275,#94276,#94277,
#94278,#94279,#94280,#94281,#94282,#94283,#94284,#94285,#94286,#94287,#94288,
#94289,#94290,#94291,#94292,#94293,#94294,#94295,#94296,#94297,#94298,#94299,
#94300,#94301,#94302,#94303,#94304,#94305,#94306,#94307,#94308,#94309,#94310,
#94311,#94312,#94313,#94314,#94315,#94316,#94317,#94318,#94319,#94320,#94321,
#94322,#94323,#94324,#94325,#94326,#94327,#94328,#94329,#94330,#94331,#94332,
#94333,#94334,#94335),.UNSPECIFIED.,.F.,.F.,(4,3,3,3,3,3,3,3,3,3,3,3,3,
3,3,3,3,3,3,3,3,3,3,3,3,3,3,3,3,3,3,3,3,3,3,3,3,3,3,4),(0.,0.0741261668227613,
0.149049466564394,0.224263098602536,0.298872907613775,0.34593069051842,
0.381224027696904,0.391900396664017,0.403121243662082,0.477602560183117,
0.487104039232354,0.561377195983551,0.635987882023318,0.710367213466364,
0.774793266715159,0.786415222382851,0.860297938446043,0.934077552859576,
0.968071426461543,1.04206547223162,1.11586018693168,1.15671188839394,1.16870781125156,
1.2419832929878,1.31537203776292,1.38812718419361,1.4426737986298,1.50108005437742,
1.52663279126701,1.54012983204117,1.55002299328553,1.57202512135779,1.64480776723829,
1.71108678658141,1.76079605108876,1.77610764643868,1.84829504471514,1.90992384461079,
1.98235653831781,1.99217144768673),.UNSPECIFIED.);
#949=SHAPE_REPRESENTATION_RELATIONSHIP('SRR','None',#94501,#964);
#964=ADVANCED_BREP_SHAPE_REPRESENTATION('',(#994),#94410);
#979=STYLED_ITEM('',(#94581),#994);
#994=MANIFOLD_SOLID_BREP('Body1',#8264);
#1050=FACE_BOUND('',#1918,.T.);
#1051=FACE_BOUND('',#1919,.T.);
#1052=FACE_BOUND('',#1920,.T.);
#1053=FACE_BOUND('',#1923,.T.);
#1054=FACE_BOUND('',#1924,.T.);
#1055=FACE_BOUND('',#1925,.T.);
#1154=PLANE('',#8910);
#1155=PLANE('',#8914);
#1493=FACE_OUTER_BOUND('',#1903,.T.);
#1494=FACE_OUTER_BOUND('',#1904,.T.);
#1495=FACE_OUTER_BOUND('',#1905,.T.);
#1496=FACE_OUTER_BOUND('',#1906,.T.);
#1497=FACE_OUTER_BOUND('',#1907,.T.);
#1498=FACE_OUTER_BOUND('',#1908,.T.);
#1499=FACE_OUTER_BOUND('',#1909,.T.);
#1500=FACE_OUTER_BOUND('',#1910,.T.);
#1501=FACE_OUTER_BOUND('',#1911,.T.);
#1502=FACE_OUTER_BOUND('',#1912,.T.);
#1503=FACE_OUTER_BOUND('',#1913,.T.);
#1504=FACE_OUTER_BOUND('',#1914,.T.);
#1505=FACE_OUTER_BOUND('',#1915,.T.);
#1506=FACE_OUTER_BOUND('',#1916,.T.);
#1507=FACE_OUTER_BOUND('',#1917,.T.);
#1508=FACE_OUTER_BOUND('',#1921,.T.);
#1509=FACE_OUTER_BOUND('',#1922,.T.);
#1903=EDGE_LOOP('',(#7538,#7539,#7540,#7541));
#1904=EDGE_LOOP('',(#7542,#7543,#7544,#7545,#7546,#7547));
#1905=EDGE_LOOP('',(#7548,#7549,#7550,#7551,#7552,#7553));
#1906=EDGE_LOOP('',(#7554,#7555,#7556,#7557,#7558,#7559));
#1907=EDGE_LOOP('',(#7560,#7561,#7562,#7563));
#1908=EDGE_LOOP('',(#7564,#7565,#7566,#7567));
#1909=EDGE_LOOP('',(#7568,#7569,#7570,#7571));
#1910=EDGE_LOOP('',(#7572,#7573,#7574,#7575));
#1911=EDGE_LOOP('',(#7576,#7577,#7578,#7579));
#1912=EDGE_LOOP('',(#7580,#7581,#7582,#7583,#7584,#7585));
#1913=EDGE_LOOP('',(#7586,#7587,#7588,#7589));
#1914=EDGE_LOOP('',(#7590,#7591,#7592,#7593));
#1915=EDGE_LOOP('',(#7594,#7595,#7596,#7597,#7598,#7599,#7600,#7601,#7602,
#7603,#7604,#7605,#7606,#7607,#7608,#7609));
#1916=EDGE_LOOP('',(#7610,#7611,#7612,#7613,#7614,#7615,#7616,#7617,#7618,
#7619,#7620,#7621,#7622,#7623,#7624,#7625,#7626));
#1917=EDGE_LOOP('',(#7627));
#1918=EDGE_LOOP('',(#7628));
#1919=EDGE_LOOP('',(#7629));
#1920=EDGE_LOOP('',(#7630,#7631,#7632,#7633));
#1921=EDGE_LOOP('',(#7634,#7635,#7636,#7637));
#1922=EDGE_LOOP('',(#7638));
#1923=EDGE_LOOP('',(#7639));
#1924=EDGE_LOOP('',(#7640));
#1925=EDGE_LOOP('',(#7641,#7642,#7643,#7644,#7645));
#2317=LINE('',#91551,#2715);
#2318=LINE('',#91575,#2716);
#2319=LINE('',#91789,#2717);
#2320=LINE('',#91925,#2718);
#2321=LINE('',#92053,#2719);
#2322=LINE('',#92200,#2720);
#2323=LINE('',#92238,#2721);
#2324=LINE('',#92650,#2722);
#2325=LINE('',#93391,#2723);
#2326=LINE('',#93397,#2724);
#2327=LINE('',#94341,#2725);
#2715=VECTOR('',#10245,10.076);
#2716=VECTOR('',#10250,10.076);
#2717=VECTOR('',#10253,10.076);
#2718=VECTOR('',#10256,10.076);
#2719=VECTOR('',#10261,9.5175);
#2720=VECTOR('',#10266,9.5175);
#2721=VECTOR('',#10269,9.5175);
#2722=VECTOR('',#10272,9.5175);
#2723=VECTOR('',#10283,1.);
#2724=VECTOR('',#10290,1.);
#2725=VECTOR('',#10299,14.);
#2832=CIRCLE('',#8891,10.076);
#2833=CIRCLE('',#8895,10.076);
#2834=CIRCLE('',#8897,9.5175);
#2835=CIRCLE('',#8901,9.5175);
#2836=CIRCLE('',#8905,1.);
#2837=CIRCLE('',#8906,1.);
#2838=CIRCLE('',#8908,1.);
#2839=CIRCLE('',#8909,1.);
#2840=CIRCLE('',#8911,14.);
#2841=CIRCLE('',#8913,14.);
#3769=VERTEX_POINT('',#91549);
#3770=VERTEX_POINT('',#91550);
#3771=VERTEX_POINT('',#91552);
#3772=VERTEX_POINT('',#91561);
#3773=VERTEX_POINT('',#91573);
#3774=VERTEX_POINT('',#91574);
#3775=VERTEX_POINT('',#91576);
#3776=VERTEX_POINT('',#91764);
#3777=VERTEX_POINT('',#91787);
#3778=VERTEX_POINT('',#91788);
#3779=VERTEX_POINT('',#91790);
#3780=VERTEX_POINT('',#91900);
#3781=VERTEX_POINT('',#91923);
#3782=VERTEX_POINT('',#91924);
#3783=VERTEX_POINT('',#91926);
#3784=VERTEX_POINT('',#92024);
#3785=VERTEX_POINT('',#92031);
#3786=VERTEX_POINT('',#92033);
#3787=VERTEX_POINT('',#92051);
#3788=VERTEX_POINT('',#92052);
#3789=VERTEX_POINT('',#92054);
#3790=VERTEX_POINT('',#92086);
#3791=VERTEX_POINT('',#92198);
#3792=VERTEX_POINT('',#92199);
#3793=VERTEX_POINT('',#92236);
#3794=VERTEX_POINT('',#92237);
#3795=VERTEX_POINT('',#92648);
#3796=VERTEX_POINT('',#92649);
#3797=VERTEX_POINT('',#92651);
#3798=VERTEX_POINT('',#92821);
#3799=VERTEX_POINT('',#93177);
#3800=VERTEX_POINT('',#93199);
#3801=VERTEX_POINT('',#93388);
#3802=VERTEX_POINT('',#93390);
#3803=VERTEX_POINT('',#93394);
#3804=VERTEX_POINT('',#93396);
#3805=VERTEX_POINT('',#94213);
#3806=VERTEX_POINT('',#94337);
#3807=VERTEX_POINT('',#94340);
#5034=EDGE_CURVE('',#3769,#3770,#2317,.T.);
#5035=EDGE_CURVE('',#3770,#3771,#903,.T.);
#5036=EDGE_CURVE('',#3772,#3771,#2832,.T.);
#5037=EDGE_CURVE('',#3769,#3772,#904,.T.);
#5038=EDGE_CURVE('',#3773,#3774,#2318,.T.);
#5039=EDGE_CURVE('',#3774,#3775,#905,.T.);
#5040=EDGE_CURVE('',#3775,#3770,#906,.T.);
#5041=EDGE_CURVE('',#3776,#3769,#907,.T.);
#5042=EDGE_CURVE('',#3773,#3776,#908,.T.);
#5043=EDGE_CURVE('',#3777,#3778,#2319,.T.);
#5044=EDGE_CURVE('',#3778,#3779,#909,.T.);
#5045=EDGE_CURVE('',#3779,#3774,#910,.T.);
#5046=EDGE_CURVE('',#3780,#3773,#911,.T.);
#5047=EDGE_CURVE('',#3777,#3780,#912,.T.);
#5048=EDGE_CURVE('',#3781,#3782,#2320,.T.);
#5049=EDGE_CURVE('',#3783,#3781,#913,.T.);
#5050=EDGE_CURVE('',#3784,#3783,#914,.T.);
#5051=EDGE_CURVE('',#3785,#3784,#2833,.T.);
#5052=EDGE_CURVE('',#3785,#3786,#915,.T.);
#5053=EDGE_CURVE('',#3786,#3782,#916,.T.);
#5054=EDGE_CURVE('',#3787,#3788,#2321,.T.);
#5055=EDGE_CURVE('',#3788,#3789,#917,.T.);
#5056=EDGE_CURVE('',#3790,#3789,#2834,.F.);
#5057=EDGE_CURVE('',#3790,#3787,#918,.T.);
#5058=EDGE_CURVE('',#3791,#3792,#2322,.T.);
#5059=EDGE_CURVE('',#3792,#3788,#919,.T.);
#5060=EDGE_CURVE('',#3787,#3791,#920,.T.);
#5061=EDGE_CURVE('',#3793,#3794,#2323,.T.);
#5062=EDGE_CURVE('',#3794,#3792,#921,.T.);
#5063=EDGE_CURVE('',#3791,#3793,#922,.T.);
#5064=EDGE_CURVE('',#3795,#3796,#2324,.T.);
#5065=EDGE_CURVE('',#3795,#3797,#923,.T.);
#5066=EDGE_CURVE('',#3797,#3798,#2835,.F.);
#5067=EDGE_CURVE('',#3798,#3796,#924,.T.);
#5068=EDGE_CURVE('',#3796,#3794,#925,.T.);
#5069=EDGE_CURVE('',#3793,#3795,#926,.T.);
#5070=EDGE_CURVE('',#3782,#3799,#927,.T.);
#5071=EDGE_CURVE('',#3799,#3778,#928,.T.);
#5072=EDGE_CURVE('',#3800,#3777,#929,.T.);
#5073=EDGE_CURVE('',#3781,#3800,#930,.T.);
#5074=EDGE_CURVE('',#3801,#3801,#2836,.T.);
#5075=EDGE_CURVE('',#3801,#3802,#2325,.T.);
#5076=EDGE_CURVE('',#3802,#3802,#2837,.T.);
#5077=EDGE_CURVE('',#3803,#3803,#2838,.T.);
#5078=EDGE_CURVE('',#3803,#3804,#2326,.T.);
#5079=EDGE_CURVE('',#3804,#3804,#2839,.T.);
#5080=EDGE_CURVE('',#3771,#3790,#931,.T.);
#5081=EDGE_CURVE('',#3797,#3785,#932,.T.);
#5082=EDGE_CURVE('',#3789,#3772,#933,.T.);
#5083=EDGE_CURVE('',#3798,#3805,#934,.T.);
#5084=EDGE_CURVE('',#3784,#3805,#935,.T.);
#5085=EDGE_CURVE('',#3806,#3806,#2840,.T.);
#5086=EDGE_CURVE('',#3806,#3807,#2327,.T.);
#5087=EDGE_CURVE('',#3807,#3807,#2841,.T.);
#7538=ORIENTED_EDGE('',*,*,#5034,.T.);
#7539=ORIENTED_EDGE('',*,*,#5035,.T.);
#7540=ORIENTED_EDGE('',*,*,#5036,.F.);
#7541=ORIENTED_EDGE('',*,*,#5037,.F.);
#7542=ORIENTED_EDGE('',*,*,#5038,.T.);
#7543=ORIENTED_EDGE('',*,*,#5039,.T.);
#7544=ORIENTED_EDGE('',*,*,#5040,.T.);
#7545=ORIENTED_EDGE('',*,*,#5034,.F.);
#7546=ORIENTED_EDGE('',*,*,#5041,.F.);
#7547=ORIENTED_EDGE('',*,*,#5042,.F.);
#7548=ORIENTED_EDGE('',*,*,#5043,.T.);
#7549=ORIENTED_EDGE('',*,*,#5044,.T.);
#7550=ORIENTED_EDGE('',*,*,#5045,.T.);
#7551=ORIENTED_EDGE('',*,*,#5038,.F.);
#7552=ORIENTED_EDGE('',*,*,#5046,.F.);
#7553=ORIENTED_EDGE('',*,*,#5047,.F.);
#7554=ORIENTED_EDGE('',*,*,#5048,.F.);
#7555=ORIENTED_EDGE('',*,*,#5049,.F.);
#7556=ORIENTED_EDGE('',*,*,#5050,.F.);
#7557=ORIENTED_EDGE('',*,*,#5051,.F.);
#7558=ORIENTED_EDGE('',*,*,#5052,.T.);
#7559=ORIENTED_EDGE('',*,*,#5053,.T.);
#7560=ORIENTED_EDGE('',*,*,#5054,.T.);
#7561=ORIENTED_EDGE('',*,*,#5055,.T.);
#7562=ORIENTED_EDGE('',*,*,#5056,.F.);
#7563=ORIENTED_EDGE('',*,*,#5057,.T.);
#7564=ORIENTED_EDGE('',*,*,#5058,.T.);
#7565=ORIENTED_EDGE('',*,*,#5059,.T.);
#7566=ORIENTED_EDGE('',*,*,#5054,.F.);
#7567=ORIENTED_EDGE('',*,*,#5060,.T.);
#7568=ORIENTED_EDGE('',*,*,#5061,.T.);
#7569=ORIENTED_EDGE('',*,*,#5062,.T.);
#7570=ORIENTED_EDGE('',*,*,#5058,.F.);
#7571=ORIENTED_EDGE('',*,*,#5063,.T.);
#7572=ORIENTED_EDGE('',*,*,#5064,.F.);
#7573=ORIENTED_EDGE('',*,*,#5065,.T.);
#7574=ORIENTED_EDGE('',*,*,#5066,.T.);
#7575=ORIENTED_EDGE('',*,*,#5067,.T.);
#7576=ORIENTED_EDGE('',*,*,#5064,.T.);
#7577=ORIENTED_EDGE('',*,*,#5068,.T.);
#7578=ORIENTED_EDGE('',*,*,#5061,.F.);
#7579=ORIENTED_EDGE('',*,*,#5069,.T.);
#7580=ORIENTED_EDGE('',*,*,#5048,.T.);
#7581=ORIENTED_EDGE('',*,*,#5070,.T.);
#7582=ORIENTED_EDGE('',*,*,#5071,.T.);
#7583=ORIENTED_EDGE('',*,*,#5043,.F.);
#7584=ORIENTED_EDGE('',*,*,#5072,.F.);
#7585=ORIENTED_EDGE('',*,*,#5073,.F.);
#7586=ORIENTED_EDGE('',*,*,#5074,.F.);
#7587=ORIENTED_EDGE('',*,*,#5075,.T.);
#7588=ORIENTED_EDGE('',*,*,#5076,.F.);
#7589=ORIENTED_EDGE('',*,*,#5075,.F.);
#7590=ORIENTED_EDGE('',*,*,#5077,.F.);
#7591=ORIENTED_EDGE('',*,*,#5078,.T.);
#7592=ORIENTED_EDGE('',*,*,#5079,.F.);
#7593=ORIENTED_EDGE('',*,*,#5078,.F.);
#7594=ORIENTED_EDGE('',*,*,#5080,.F.);
#7595=ORIENTED_EDGE('',*,*,#5035,.F.);
#7596=ORIENTED_EDGE('',*,*,#5040,.F.);
#7597=ORIENTED_EDGE('',*,*,#5039,.F.);
#7598=ORIENTED_EDGE('',*,*,#5045,.F.);
#7599=ORIENTED_EDGE('',*,*,#5044,.F.);
#7600=ORIENTED_EDGE('',*,*,#5071,.F.);
#7601=ORIENTED_EDGE('',*,*,#5070,.F.);
#7602=ORIENTED_EDGE('',*,*,#5053,.F.);
#7603=ORIENTED_EDGE('',*,*,#5052,.F.);
#7604=ORIENTED_EDGE('',*,*,#5081,.F.);
#7605=ORIENTED_EDGE('',*,*,#5065,.F.);
#7606=ORIENTED_EDGE('',*,*,#5069,.F.);
#7607=ORIENTED_EDGE('',*,*,#5063,.F.);
#7608=ORIENTED_EDGE('',*,*,#5060,.F.);
#7609=ORIENTED_EDGE('',*,*,#5057,.F.);
#7610=ORIENTED_EDGE('',*,*,#5082,.F.);
#7611=ORIENTED_EDGE('',*,*,#5055,.F.);
#7612=ORIENTED_EDGE('',*,*,#5059,.F.);
#7613=ORIENTED_EDGE('',*,*,#5062,.F.);
#7614=ORIENTED_EDGE('',*,*,#5068,.F.);
#7615=ORIENTED_EDGE('',*,*,#5067,.F.);
#7616=ORIENTED_EDGE('',*,*,#5083,.T.);
#7617=ORIENTED_EDGE('',*,*,#5084,.F.);
#7618=ORIENTED_EDGE('',*,*,#5050,.T.);
#7619=ORIENTED_EDGE('',*,*,#5049,.T.);
#7620=ORIENTED_EDGE('',*,*,#5073,.T.);
#7621=ORIENTED_EDGE('',*,*,#5072,.T.);
#7622=ORIENTED_EDGE('',*,*,#5047,.T.);
#7623=ORIENTED_EDGE('',*,*,#5046,.T.);
#7624=ORIENTED_EDGE('',*,*,#5042,.T.);
#7625=ORIENTED_EDGE('',*,*,#5041,.T.);
#7626=ORIENTED_EDGE('',*,*,#5037,.T.);
#7627=ORIENTED_EDGE('',*,*,#5085,.T.);
#7628=ORIENTED_EDGE('',*,*,#5074,.T.);
#7629=ORIENTED_EDGE('',*,*,#5077,.T.);
#7630=ORIENTED_EDGE('',*,*,#5082,.T.);
#7631=ORIENTED_EDGE('',*,*,#5036,.T.);
#7632=ORIENTED_EDGE('',*,*,#5080,.T.);
#7633=ORIENTED_EDGE('',*,*,#5056,.T.);
#7634=ORIENTED_EDGE('',*,*,#5085,.F.);
#7635=ORIENTED_EDGE('',*,*,#5086,.T.);
#7636=ORIENTED_EDGE('',*,*,#5087,.T.);
#7637=ORIENTED_EDGE('',*,*,#5086,.F.);
#7638=ORIENTED_EDGE('',*,*,#5087,.F.);
#7639=ORIENTED_EDGE('',*,*,#5076,.T.);
#7640=ORIENTED_EDGE('',*,*,#5079,.T.);
#7641=ORIENTED_EDGE('',*,*,#5084,.T.);
#7642=ORIENTED_EDGE('',*,*,#5083,.F.);
#7643=ORIENTED_EDGE('',*,*,#5066,.F.);
#7644=ORIENTED_EDGE('',*,*,#5081,.T.);
#7645=ORIENTED_EDGE('',*,*,#5051,.T.);
#7880=CYLINDRICAL_SURFACE('',#8890,10.076);
#7881=CYLINDRICAL_SURFACE('',#8892,10.076);
#7882=CYLINDRICAL_SURFACE('',#8893,10.076);
#7883=CYLINDRICAL_SURFACE('',#8894,10.076);
#7884=CYLINDRICAL_SURFACE('',#8896,9.5175);
#7885=CYLINDRICAL_SURFACE('',#8898,9.5175);
#7886=CYLINDRICAL_SURFACE('',#8899,9.5175);
#7887=CYLINDRICAL_SURFACE('',#8900,9.5175);
#7888=CYLINDRICAL_SURFACE('',#8902,9.5175);
#7889=CYLINDRICAL_SURFACE('',#8903,10.076);
#7890=CYLINDRICAL_SURFACE('',#8904,1.);
#7891=CYLINDRICAL_SURFACE('',#8907,1.);
#7892=CYLINDRICAL_SURFACE('',#8912,14.);
#8230=ADVANCED_FACE('',(#1493),#7880,.F.);
#8231=ADVANCED_FACE('',(#1494),#7881,.F.);
#8232=ADVANCED_FACE('',(#1495),#7882,.F.);
#8233=ADVANCED_FACE('',(#1496),#7883,.F.);
#8234=ADVANCED_FACE('',(#1497),#7884,.F.);
#8235=ADVANCED_FACE('',(#1498),#7885,.F.);
#8236=ADVANCED_FACE('',(#1499),#7886,.F.);
#8237=ADVANCED_FACE('',(#1500),#7887,.F.);
#8238=ADVANCED_FACE('',(#1501),#7888,.F.);
#8239=ADVANCED_FACE('',(#1502),#7889,.F.);
#8240=ADVANCED_FACE('',(#1503),#7890,.F.);
#8241=ADVANCED_FACE('',(#1504),#7891,.F.);
#8242=ADVANCED_FACE('',(#1505),#168,.F.);
#8243=ADVANCED_FACE('',(#1506),#169,.F.);
#8244=ADVANCED_FACE('',(#1507,#1050,#1051,#1052),#1154,.T.);
#8245=ADVANCED_FACE('',(#1508),#7892,.T.);
#8246=ADVANCED_FACE('',(#1509,#1053,#1054,#1055),#1155,.F.);
#8264=CLOSED_SHELL('',(#8230,#8231,#8232,#8233,#8234,#8235,#8236,#8237,
#8238,#8239,#8240,#8241,#8242,#8243,#8244,#8245,#8246));
#8889=AXIS2_PLACEMENT_3D('',#91547,#10241,#10242);
#8890=AXIS2_PLACEMENT_3D('',#91548,#10243,#10244);
#8891=AXIS2_PLACEMENT_3D('',#91562,#10246,#10247);
#8892=AXIS2_PLACEMENT_3D('',#91572,#10248,#10249);
#8893=AXIS2_PLACEMENT_3D('',#91786,#10251,#10252);
#8894=AXIS2_PLACEMENT_3D('',#91922,#10254,#10255);
#8895=AXIS2_PLACEMENT_3D('',#92032,#10257,#10258);
#8896=AXIS2_PLACEMENT_3D('',#92050,#10259,#10260);
#8897=AXIS2_PLACEMENT_3D('',#92087,#10262,#10263);
#8898=AXIS2_PLACEMENT_3D('',#92197,#10264,#10265);
#8899=AXIS2_PLACEMENT_3D('',#92235,#10267,#10268);
#8900=AXIS2_PLACEMENT_3D('',#92647,#10270,#10271);
#8901=AXIS2_PLACEMENT_3D('',#92822,#10273,#10274);
#8902=AXIS2_PLACEMENT_3D('',#92937,#10275,#10276);
#8903=AXIS2_PLACEMENT_3D('',#93176,#10277,#10278);
#8904=AXIS2_PLACEMENT_3D('',#93387,#10279,#10280);
#8905=AXIS2_PLACEMENT_3D('',#93389,#10281,#10282);
#8906=AXIS2_PLACEMENT_3D('',#93392,#10284,#10285);
#8907=AXIS2_PLACEMENT_3D('',#93393,#10286,#10287);
#8908=AXIS2_PLACEMENT_3D('',#93395,#10288,#10289);
#8909=AXIS2_PLACEMENT_3D('',#93398,#10291,#10292);
#8910=AXIS2_PLACEMENT_3D('',#94336,#10293,#10294);
#8911=AXIS2_PLACEMENT_3D('',#94338,#10295,#10296);
#8912=AXIS2_PLACEMENT_3D('',#94339,#10297,#10298);
#8913=AXIS2_PLACEMENT_3D('',#94342,#10300,#10301);
#8914=AXIS2_PLACEMENT_3D('',#94343,#10302,#10303);
#10241=DIRECTION('axis',(0.,0.,1.));
#10242=DIRECTION('refdir',(1.,0.,0.));
#10243=DIRECTION('center_axis',(0.,0.,1.));
#10244=DIRECTION('ref_axis',(-0.608987077531584,0.793180143094581,0.));
#10245=DIRECTION('',(0.,0.,1.));
#10246=DIRECTION('center_axis',(0.,0.,-1.));
#10247=DIRECTION('ref_axis',(1.,3.67286437305492E-16,0.));
#10248=DIRECTION('center_axis',(0.,0.,1.));
#10249=DIRECTION('ref_axis',(-0.608987077531584,0.793180143094581,0.));
#10250=DIRECTION('',(0.,0.,1.));
#10251=DIRECTION('center_axis',(0.,0.,1.));
#10252=DIRECTION('ref_axis',(-0.608987077531584,0.793180143094581,0.));
#10253=DIRECTION('',(0.,0.,1.));
#10254=DIRECTION('center_axis',(0.,0.,1.));
#10255=DIRECTION('ref_axis',(-0.608987077531584,0.793180143094581,0.));
#10256=DIRECTION('',(0.,0.,1.));
#10257=DIRECTION('center_axis',(0.,0.,1.));
#10258=DIRECTION('ref_axis',(1.,3.67286437305492E-16,0.));
#10259=DIRECTION('center_axis',(0.,0.,1.));
#10260=DIRECTION('ref_axis',(1.,0.,0.));
#10261=DIRECTION('',(0.,0.,1.));
#10262=DIRECTION('center_axis',(0.,0.,1.));
#10263=DIRECTION('ref_axis',(1.,0.,0.));
#10264=DIRECTION('center_axis',(0.,0.,1.));
#10265=DIRECTION('ref_axis',(1.,0.,0.));
#10266=DIRECTION('',(0.,0.,1.));
#10267=DIRECTION('center_axis',(0.,0.,1.));
#10268=DIRECTION('ref_axis',(1.,0.,0.));
#10269=DIRECTION('',(0.,0.,1.));
#10270=DIRECTION('center_axis',(0.,0.,1.));
#10271=DIRECTION('ref_axis',(1.,0.,0.));
#10272=DIRECTION('',(0.,0.,1.));
#10273=DIRECTION('center_axis',(0.,0.,1.));
#10274=DIRECTION('ref_axis',(1.,0.,0.));
#10275=DIRECTION('center_axis',(0.,0.,1.));
#10276=DIRECTION('ref_axis',(1.,0.,0.));
#10277=DIRECTION('center_axis',(0.,0.,1.));
#10278=DIRECTION('ref_axis',(-0.608987077531584,0.793180143094581,0.));
#10279=DIRECTION('center_axis',(0.,0.,-1.));
#10280=DIRECTION('ref_axis',(1.,0.,0.));
#10281=DIRECTION('center_axis',(0.,0.,-1.));
#10282=DIRECTION('ref_axis',(1.,0.,0.));
#10283=DIRECTION('',(0.,0.,-1.));
#10284=DIRECTION('center_axis',(0.,0.,1.));
#10285=DIRECTION('ref_axis',(1.,0.,0.));
#10286=DIRECTION('center_axis',(0.,0.,-1.));
#10287=DIRECTION('ref_axis',(1.,0.,0.));
#10288=DIRECTION('center_axis',(0.,0.,-1.));
#10289=DIRECTION('ref_axis',(1.,0.,0.));
#10290=DIRECTION('',(0.,0.,-1.));
#10291=DIRECTION('center_axis',(0.,0.,1.));
#10292=DIRECTION('ref_axis',(1.,0.,0.));
#10293=DIRECTION('center_axis',(0.,0.,1.));
#10294=DIRECTION('ref_axis',(1.,0.,0.));
#10295=DIRECTION('center_axis',(0.,0.,1.));
#10296=DIRECTION('ref_axis',(1.,0.,0.));
#10297=DIRECTION('center_axis',(0.,0.,1.));
#10298=DIRECTION('ref_axis',(1.,0.,0.));
#10299=DIRECTION('',(0.,0.,-1.));
#10300=DIRECTION('center_axis',(0.,0.,1.));
#10301=DIRECTION('ref_axis',(1.,0.,0.));
#10302=DIRECTION('center_axis',(0.,0.,1.));
#10303=DIRECTION('ref_axis',(1.,0.,0.));
#91547=CARTESIAN_POINT('',(0.,0.,0.));
#91548=CARTESIAN_POINT('Origin',(0.,0.,-2.20842344717745));
#91549=CARTESIAN_POINT('',(6.1363657837075,-7.99235873417456,3.56263847785126));
#91550=CARTESIAN_POINT('',(6.13575050161833,-7.99155833647621,3.64579035276345));
#91551=CARTESIAN_POINT('',(6.13615379320824,-7.992083121821,-2.20842344717745));
#91552=CARTESIAN_POINT('',(2.60234962446753,9.73414364143214,4.));
#91553=CARTESIAN_POINT('Ctrl Pts',(6.13575050161833,-7.99155833647621,3.64579035276345));
#91554=CARTESIAN_POINT('Ctrl Pts',(6.89661927295215,-7.40686050907605,3.66094475600081));
#91555=CARTESIAN_POINT('Ctrl Pts',(8.72642379835497,-5.53871638815614,3.70182802903188));
#91556=CARTESIAN_POINT('Ctrl Pts',(10.3690110414678,-1.51793686145572,3.76844017185666));
#91557=CARTESIAN_POINT('Ctrl Pts',(9.88113494348103,3.49068484817476,3.84562678123777));
#91558=CARTESIAN_POINT('Ctrl Pts',(7.11402078469617,7.69533055119267,3.92281339061889));
#91559=CARTESIAN_POINT('Ctrl Pts',(4.1759640497451,9.31344973557609,3.97427113020629));
#91560=CARTESIAN_POINT('Ctrl Pts',(2.6023496244676,9.73414364143212,4.));
#91561=CARTESIAN_POINT('',(-2.60241879177085,9.73440315357327,3.99999685169366));
#91562=CARTESIAN_POINT('Origin',(0.,0.,4.));
#91563=CARTESIAN_POINT('Ctrl Pts',(6.1363657837075,-7.99235873417456,3.56263847785126));
#91564=CARTESIAN_POINT('Ctrl Pts',(7.2256962454093,-7.15441785607105,3.58434919887163));
#91565=CARTESIAN_POINT('Ctrl Pts',(9.23098036694038,-4.83331139710073,3.6317887896857));
#91566=CARTESIAN_POINT('Ctrl Pts',(10.4771042016857,-0.228210237258418,
3.70495725029349));
#91567=CARTESIAN_POINT('Ctrl Pts',(9.37532803384437,4.68240093714628,3.7821438596746));
#91568=CARTESIAN_POINT('Ctrl Pts',(6.11133502294712,8.51314763294832,3.85933046905572));
#91569=CARTESIAN_POINT('Ctrl Pts',(1.71450917131053,10.2699119982464,3.93194813306207));
#91570=CARTESIAN_POINT('Ctrl Pts',(-1.30803602033293,10.0791359541843,3.97883692727472));
#91571=CARTESIAN_POINT('Ctrl Pts',(-2.60241879177086,9.73440315357327,3.99999685169366));
#91572=CARTESIAN_POINT('Origin',(0.,0.,-2.20842344717745));
#91573=CARTESIAN_POINT('',(6.1362409016225,-7.9921963794308,2.56263886265602));
#91574=CARTESIAN_POINT('',(6.13615379320825,-7.992083121821,2.64578903198487));
#91575=CARTESIAN_POINT('',(6.13615379320824,-7.992083121821,-2.20842344717745));
#91576=CARTESIAN_POINT('',(-10.0759999978312,-0.000209059053492667,3.29157655282254));
#91577=CARTESIAN_POINT('Ctrl Pts',(6.13615379320825,-7.99208312182099,2.64578903198487));
#91578=CARTESIAN_POINT('Ctrl Pts',(6.33194935528241,-7.84175539592005,2.64968751815102));
#91579=CARTESIAN_POINT('Ctrl Pts',(6.52222043055739,-7.68422727429467,2.65358600431717));
#91580=CARTESIAN_POINT('Ctrl Pts',(6.70644559174884,-7.51993108511724,2.65748449048332));
#91581=CARTESIAN_POINT('Ctrl Pts',(6.89066877557437,-7.35563665939972,2.66138293480539));
#91582=CARTESIAN_POINT('Ctrl Pts',(7.06884596855911,-7.18457449847276,2.66528137912746));
#91583=CARTESIAN_POINT('Ctrl Pts',(7.24049064021804,-7.00721565879879,2.66917982344952));
#91584=CARTESIAN_POINT('Ctrl Pts',(7.41216962074527,-6.82982136809093,2.67307904700471));
#91585=CARTESIAN_POINT('Ctrl Pts',(7.577313276671,-6.64612808368434,2.67697827055989));
#91586=CARTESIAN_POINT('Ctrl Pts',(7.73547266915676,-6.45664298104897,2.68087749411508));
#91587=CARTESIAN_POINT('Ctrl Pts',(7.82944273932568,-6.34406080612556,2.68319420958373));
#91588=CARTESIAN_POINT('Ctrl Pts',(7.92094801835551,-6.22943471971775,2.68551092505239));
#91589=CARTESIAN_POINT('Ctrl Pts',(8.00990108241083,-6.11287662643324,2.68782764052105));
#91590=CARTESIAN_POINT('Ctrl Pts',(8.15961682553693,-5.91669921828237,2.69172687414144));
#91591=CARTESIAN_POINT('Ctrl Pts',(8.30214348409879,-5.71499078402337,2.69562610776184));
#91592=CARTESIAN_POINT('Ctrl Pts',(8.43708493598507,-5.50830044414553,2.69952534138223));
#91593=CARTESIAN_POINT('Ctrl Pts',(8.5720042784268,-5.30164396938878,2.70342393613378));
#91594=CARTESIAN_POINT('Ctrl Pts',(8.69934074296439,-5.09000745174317,2.70732253088533));
#91595=CARTESIAN_POINT('Ctrl Pts',(8.81874158981831,-4.87396889321309,2.71122112563688));
#91596=CARTESIAN_POINT('Ctrl Pts',(8.93813026163517,-4.65795236365119,2.71511932285745));
#91597=CARTESIAN_POINT('Ctrl Pts',(9.0495847967984,-4.43753493328373,2.71901752007802));
#91598=CARTESIAN_POINT('Ctrl Pts',(9.15279795110948,-4.21332002892803,2.72291571729859));
#91599=CARTESIAN_POINT('Ctrl Pts',(9.25601879101199,-3.98908842879206,2.72681420479177));
#91600=CARTESIAN_POINT('Ctrl Pts',(9.35099690476323,-3.76105904159036,2.73071269228494));
#91601=CARTESIAN_POINT('Ctrl Pts',(9.43747229274958,-3.52985732340331,2.73461117977812));
#91602=CARTESIAN_POINT('Ctrl Pts',(9.52394672476821,-3.29865816110396,2.73850962417431));
#91603=CARTESIAN_POINT('Ctrl Pts',(9.60191852337963,-3.06428699969025,2.74240806857051));
#91604=CARTESIAN_POINT('Ctrl Pts',(9.67117660924036,-2.82738730860881,2.7463065129667));
#91605=CARTESIAN_POINT('Ctrl Pts',(9.74044856055598,-2.59044019025672,2.75020573783068));
#91606=CARTESIAN_POINT('Ctrl Pts',(9.80100323464222,-2.35096379811987,2.75410496269466));
#91607=CARTESIAN_POINT('Ctrl Pts',(9.85267964124371,-2.10961605203928,2.75800418755864));
#91608=CARTESIAN_POINT('Ctrl Pts',(9.88364774769249,-1.96498365239441,2.76034087500648));
#91609=CARTESIAN_POINT('Ctrl Pts',(9.91142842287093,-1.81967945557351,2.76267756245433));
#91610=CARTESIAN_POINT('Ctrl Pts',(9.93599580785843,-1.67384685865215,2.76501424990217));
#91611=CARTESIAN_POINT('Ctrl Pts',(9.97699142497022,-1.43049587486422,2.76891348231826));
#91612=CARTESIAN_POINT('Ctrl Pts',(10.0090484682785,-1.18560314388318,2.77281271473435));
#91613=CARTESIAN_POINT('Ctrl Pts',(10.0320724880943,-0.939839131778517,
2.77671194715044));
#91614=CARTESIAN_POINT('Ctrl Pts',(10.0550927355203,-0.694115387083012,
2.78061054069355));
#91615=CARTESIAN_POINT('Ctrl Pts',(10.0690828880855,-0.447520923549086,
2.78450913423665));
#91616=CARTESIAN_POINT('Ctrl Pts',(10.0740003400475,-0.200731533953737,
2.78840772777976));
#91617=CARTESIAN_POINT('Ctrl Pts',(10.078917290587,0.0460326910366703,2.79230592379132));
#91618=CARTESIAN_POINT('Ctrl Pts',(10.0747633822627,0.292991523916393,2.79620411980289));
#91619=CARTESIAN_POINT('Ctrl Pts',(10.0615481113648,0.539467888470903,2.80010231581446));
#91620=CARTESIAN_POINT('Ctrl Pts',(10.0483318563879,0.785962606958579,2.80400080210631));
#91621=CARTESIAN_POINT('Ctrl Pts',(10.0260529026826,1.0319745069307,2.80789928839816));
#91622=CARTESIAN_POINT('Ctrl Pts',(9.99477281292278,1.27682904809517,2.81179777469001));
#91623=CARTESIAN_POINT('Ctrl Pts',(9.96349306890727,1.52168088283989,2.81569621789121));
#91624=CARTESIAN_POINT('Ctrl Pts',(9.92321242523012,1.76537510822755,2.81959466109241));
#91625=CARTESIAN_POINT('Ctrl Pts',(9.87404412123745,2.00724405388487,2.82349310429362));
#91626=CARTESIAN_POINT('Ctrl Pts',(9.8248659735366,2.24916142275643,2.82739232798009));
#91627=CARTESIAN_POINT('Ctrl Pts',(9.76679666510075,2.4892525084711,2.83129155166657));
#91628=CARTESIAN_POINT('Ctrl Pts',(9.70000048496686,2.72686020757258,2.83519077535305));
#91629=CARTESIAN_POINT('Ctrl Pts',(9.65997142049938,2.86925179173558,2.83752746999646));
#91630=CARTESIAN_POINT('Ctrl Pts',(9.61680927882901,3.01075175524593,2.83986416463987));
#91631=CARTESIAN_POINT('Ctrl Pts',(9.57055803349138,3.15122118036384,2.84220085928328));
#91632=CARTESIAN_POINT('Ctrl Pts',(9.49337873111043,3.38562205232547,2.8461000940204));
#91633=CARTESIAN_POINT('Ctrl Pts',(9.40757284882014,3.61721981916801,2.84999932875753));
#91634=CARTESIAN_POINT('Ctrl Pts',(9.31336939248879,3.84537729736016,2.85389856349465));
#91635=CARTESIAN_POINT('Ctrl Pts',(9.21918137083707,4.07349739329779,2.8577971593652));
#91636=CARTESIAN_POINT('Ctrl Pts',(9.11659862816643,4.29817806842485,2.86169575523576));
#91637=CARTESIAN_POINT('Ctrl Pts',(9.00589851916906,4.51880159582477,2.86559435110631));
#91638=CARTESIAN_POINT('Ctrl Pts',(8.89520969803949,4.73940262668668,2.86949254944487));
#91639=CARTESIAN_POINT('Ctrl Pts',(8.77640528827373,4.95594708693956,2.87339074778343));
#91640=CARTESIAN_POINT('Ctrl Pts',(8.64980933678775,5.16784040361344,2.87728894612199));
#91641=CARTESIAN_POINT('Ctrl Pts',(8.52320395885865,5.3797494980454,2.88118743472375));
#91642=CARTESIAN_POINT('Ctrl Pts',(8.38880602045493,5.58700651623069,2.8850859233255));
#91643=CARTESIAN_POINT('Ctrl Pts',(8.24698444863633,5.7890434014568,2.88898441192725));
#91644=CARTESIAN_POINT('Ctrl Pts',(8.1051644448861,5.99107805283623,2.89288285742487));
#91645=CARTESIAN_POINT('Ctrl Pts',(7.95592113370849,6.18789245983946,2.89678130292248));
#91646=CARTESIAN_POINT('Ctrl Pts',(7.79966595708087,6.37894873454504,2.9006797484201));
#91647=CARTESIAN_POINT('Ctrl Pts',(7.64337949893426,6.57004325777854,2.90457897436735));
#91648=CARTESIAN_POINT('Ctrl Pts',(7.48007854648031,6.75537712924579,2.90847820031461));
#91649=CARTESIAN_POINT('Ctrl Pts',(7.31021477843386,6.93444560820598,2.91237742626187));
#91650=CARTESIAN_POINT('Ctrl Pts',(7.20842088115244,7.04175559292638,2.91471410706271));
#91651=CARTESIAN_POINT('Ctrl Pts',(7.10427088804325,7.14681619519958,2.91705078786355));
#91652=CARTESIAN_POINT('Ctrl Pts',(6.99786846178245,7.24952501834365,2.91938746866439));
#91653=CARTESIAN_POINT('Ctrl Pts',(6.82031418339718,7.42091576212657,2.92328669998824));
#91654=CARTESIAN_POINT('Ctrl Pts',(6.63643488235327,7.58580503799604,2.92718593131208));
#91655=CARTESIAN_POINT('Ctrl Pts',(6.44673020355477,7.74373589958843,2.93108516263593));
#91656=CARTESIAN_POINT('Ctrl Pts',(6.2570566070791,7.90164088486583,2.93498375508694));
#91657=CARTESIAN_POINT('Ctrl Pts',(6.06155975231665,8.05258955369743,2.93888234753795));
#91658=CARTESIAN_POINT('Ctrl Pts',(5.86077298722548,8.19616471236445,2.94278093998896));
#91659=CARTESIAN_POINT('Ctrl Pts',(5.66000669578056,8.3397252310874,2.94667913491177));
#91660=CARTESIAN_POINT('Ctrl Pts',(5.45395179764753,8.4759135789366,2.95057732983457));
#91661=CARTESIAN_POINT('Ctrl Pts',(5.24317215460739,8.60435481353191,2.95447552475737));
#91662=CARTESIAN_POINT('Ctrl Pts',(5.03237681511165,8.73280561296046,2.95837400997312));
#91663=CARTESIAN_POINT('Ctrl Pts',(4.81685626416003,8.85350799896822,2.96227249518887));
#91664=CARTESIAN_POINT('Ctrl Pts',(4.5972017067638,8.96613141033122,2.96617098040462));
#91665=CARTESIAN_POINT('Ctrl Pts',(4.37754957674429,9.07875357710612,2.97006942253867));
#91666=CARTESIAN_POINT('Ctrl Pts',(4.1537637805712,9.18329682254549,2.97396786467271));
#91667=CARTESIAN_POINT('Ctrl Pts',(3.92645907121909,9.2794770952916,2.97786630680676));
#91668=CARTESIAN_POINT('Ctrl Pts',(3.69910885325884,9.37567662426146,2.98176552944674));
#91669=CARTESIAN_POINT('Ctrl Pts',(3.46823857085602,9.46350972581889,2.98566475208673));
#91670=CARTESIAN_POINT('Ctrl Pts',(3.23448312098629,9.54274043134648,2.98956397472671));
#91671=CARTESIAN_POINT('Ctrl Pts',(3.09439965596286,9.59022129980426,2.99190067583298));
#91672=CARTESIAN_POINT('Ctrl Pts',(2.95328040588612,9.6346137339204,2.99423737693925));
#91673=CARTESIAN_POINT('Ctrl Pts',(2.81126481955898,9.67587547017375,2.99657407804552));
#91674=CARTESIAN_POINT('Ctrl Pts',(2.57428456164226,9.74472859504756,3.00047331224339));
#91675=CARTESIAN_POINT('Ctrl Pts',(2.33473955692088,9.80488130013986,3.00437254644126));
#91676=CARTESIAN_POINT('Ctrl Pts',(2.09328485806413,9.85616226038307,3.00827178063913));
#91677=CARTESIAN_POINT('Ctrl Pts',(1.85186972071869,9.90743481841957,3.01217037596107));
#91678=CARTESIAN_POINT('Ctrl Pts',(1.60854578631715,9.94983847561576,3.016068971283));
#91679=CARTESIAN_POINT('Ctrl Pts',(1.36397939188466,9.98325278746932,3.01996756660493));
#91680=CARTESIAN_POINT('Ctrl Pts',(1.11943793588059,10.0166636920664,3.02386576438721));
#91681=CARTESIAN_POINT('Ctrl Pts',(0.873654548801523,10.0410870439685,3.02776396216948));
#91682=CARTESIAN_POINT('Ctrl Pts',(0.627302865707757,10.0564540030109,3.03166215995176));
#91683=CARTESIAN_POINT('Ctrl Pts',(0.380932839531959,10.0718221062607,3.03556064798966));
#91684=CARTESIAN_POINT('Ctrl Pts',(0.133994710725798,10.078132449085,3.03945913602756));
#91685=CARTESIAN_POINT('Ctrl Pts',(-0.112834385489892,10.0753682017806,
3.04335762406546));
#91686=CARTESIAN_POINT('Ctrl Pts',(-0.359660752396465,10.0726039850418,
3.04725606899589));
#91687=CARTESIAN_POINT('Ctrl Pts',(-0.606377810516523,10.060765384096,3.05115451392631));
#91688=CARTESIAN_POINT('Ctrl Pts',(-0.852309274447887,10.0398876936294,
3.05505295885674));
#91689=CARTESIAN_POINT('Ctrl Pts',(-1.09828997256641,10.0190058235588,3.05895218423536));
#91690=CARTESIAN_POINT('Ctrl Pts',(-1.3434844844748,9.98908127118697,3.06285140961398));
#91691=CARTESIAN_POINT('Ctrl Pts',(-1.587221119285,9.9502012602005,3.06675063499261));
#91692=CARTESIAN_POINT('Ctrl Pts',(-1.73328488188769,9.92690168236256,3.06908731913728));
#91693=CARTESIAN_POINT('Ctrl Pts',(-1.87882520253984,9.90038698736819,3.07142400328195));
#91694=CARTESIAN_POINT('Ctrl Pts',(-2.02369901335421,9.87068479404287,3.07376068742663));
#91695=CARTESIAN_POINT('Ctrl Pts',(-2.2654507249401,9.82112058341097,3.07765992489568));
#91696=CARTESIAN_POINT('Ctrl Pts',(-2.50541538755697,9.76266356830015,3.08155916236472));
#91697=CARTESIAN_POINT('Ctrl Pts',(-2.74293361492496,9.69546755881916,3.08545839983376));
#91698=CARTESIAN_POINT('Ctrl Pts',(-2.98041292794163,9.6282825585527,3.08935699846217));
#91699=CARTESIAN_POINT('Ctrl Pts',(-3.21544633787951,9.55236149802127,3.09325559709058));
#91700=CARTESIAN_POINT('Ctrl Pts',(-3.44738819534,9.46790846125111,3.09715419571898));
#91701=CARTESIAN_POINT('Ctrl Pts',(-3.6793064032186,9.38346403560027,3.10105239683299));
#91702=CARTESIAN_POINT('Ctrl Pts',(-3.90813342633422,9.29048946612366,3.10495059794699));
#91703=CARTESIAN_POINT('Ctrl Pts',(-4.13324121621327,9.18923789269795,3.108848799061));
#91704=CARTESIAN_POINT('Ctrl Pts',(-4.35836576819106,9.08797877982249,3.11274729044498));
#91705=CARTESIAN_POINT('Ctrl Pts',(-4.57977027827707,8.97844154322405,3.11664578182896));
#91706=CARTESIAN_POINT('Ctrl Pts',(-4.79684784816732,8.86092696739639,3.12054427321294));
#91707=CARTESIAN_POINT('Ctrl Pts',(-5.01392301786911,8.7434136909067,3.12444272149198));
#91708=CARTESIAN_POINT('Ctrl Pts',(-5.22667109902227,8.61792338611242,3.12834116977103));
#91709=CARTESIAN_POINT('Ctrl Pts',(-5.43451024495873,8.48480255500613,3.13223961805008));
#91710=CARTESIAN_POINT('Ctrl Pts',(-5.64239099821483,8.35165507444002,3.13613884675951));
#91711=CARTESIAN_POINT('Ctrl Pts',(-5.84536061763127,8.21087416514267,3.14003807546894));
#91712=CARTESIAN_POINT('Ctrl Pts',(-6.04286552996029,8.06285012801415,3.14393730417836));
#91713=CARTESIAN_POINT('Ctrl Pts',(-6.16122295248895,7.97414477228288,3.14627396838816));
#91714=CARTESIAN_POINT('Ctrl Pts',(-6.27761847520027,7.88283911723174,3.14861063259795));
#91715=CARTESIAN_POINT('Ctrl Pts',(-6.39193840660977,7.78902429102047,3.15094729680774));
#91716=CARTESIAN_POINT('Ctrl Pts',(-6.58270521411611,7.63247455667032,3.15484651163424));
#91717=CARTESIAN_POINT('Ctrl Pts',(-6.76774539581126,7.4688906653599,3.15874572646074));
#91718=CARTESIAN_POINT('Ctrl Pts',(-6.94654731124955,7.29871608247448,3.16264494128724));
#91719=CARTESIAN_POINT('Ctrl Pts',(-7.12531992698819,7.12856938555525,3.16654351716185));
#91720=CARTESIAN_POINT('Ctrl Pts',(-7.29785611545559,6.95183434509883,3.17044209303645));
#91721=CARTESIAN_POINT('Ctrl Pts',(-7.46367982602414,6.76899249922766,3.17434066891105));
#91722=CARTESIAN_POINT('Ctrl Pts',(-7.62948662668822,6.58616929868853,3.17823884722764));
#91723=CARTESIAN_POINT('Ctrl Pts',(-7.78858212915114,6.3972407425548,3.18213702554422));
#91724=CARTESIAN_POINT('Ctrl Pts',(-7.94052872327196,6.2027235626693,3.18603520386081));
#91725=CARTESIAN_POINT('Ctrl Pts',(-8.09248663550991,6.00819189369153,3.18993367254283));
#91726=CARTESIAN_POINT('Ctrl Pts',(-8.23729440162687,5.80807098703512,3.19383214122485));
#91727=CARTESIAN_POINT('Ctrl Pts',(-8.37455533405834,5.60290986513214,3.19773060990687));
#91728=CARTESIAN_POINT('Ctrl Pts',(-8.51181475203737,5.39775100685039,3.20162903557559));
#91729=CARTESIAN_POINT('Ctrl Pts',(-8.6415273496758,5.18755227732144,3.20552746124431));
#91730=CARTESIAN_POINT('Ctrl Pts',(-8.76333991521675,4.9728914657741,3.20942588691303));
#91731=CARTESIAN_POINT('Ctrl Pts',(-8.88517687554087,4.75818766519742,3.21332509329964));
#91732=CARTESIAN_POINT('Ctrl Pts',(-8.99911050445519,4.53902023920256,3.21722429968625));
#91733=CARTESIAN_POINT('Ctrl Pts',(-9.10483302185017,4.31599254450547,3.22112350607286));
#91734=CARTESIAN_POINT('Ctrl Pts',(-9.16819267974994,4.18233172383667,3.22346030611153));
#91735=CARTESIAN_POINT('Ctrl Pts',(-9.22860410251766,4.04728490777612,3.22579710615019));
#91736=CARTESIAN_POINT('Ctrl Pts',(-9.28600918186325,3.91098574202865,3.22813390618886));
#91737=CARTESIAN_POINT('Ctrl Pts',(-9.38143382290358,3.68441521701905,3.23201837612452));
#91738=CARTESIAN_POINT('Ctrl Pts',(-9.46857807619525,3.45431307415355,3.23590284606019));
#91739=CARTESIAN_POINT('Ctrl Pts',(-9.54719691433382,3.22130518252072,3.23978731599585));
#91740=CARTESIAN_POINT('Ctrl Pts',(-9.62580180803594,2.98833861894379,3.24367109695232));
#91741=CARTESIAN_POINT('Ctrl Pts',(-9.69588421470461,2.75246760335617,3.24755487790879));
#91742=CARTESIAN_POINT('Ctrl Pts',(-9.75724831562987,2.51433516205339,3.25143865886526));
#91743=CARTESIAN_POINT('Ctrl Pts',(-9.8186109875981,2.27620826602907,3.25532234938194));
#91744=CARTESIAN_POINT('Ctrl Pts',(-9.87125568580342,2.03582032264973,3.25920603989862));
#91745=CARTESIAN_POINT('Ctrl Pts',(-9.91503696250514,1.79382775989134,3.2630897304153));
#91746=CARTESIAN_POINT('Ctrl Pts',(-9.95881591686286,1.5518480334415,3.26697321492462));
#91747=CARTESIAN_POINT('Ctrl Pts',(-9.99373233985306,1.30826413626401,3.27085669943393));
#91748=CARTESIAN_POINT('Ctrl Pts',(-10.0196920909372,1.06374169929095,3.27474018394325));
#91749=CARTESIAN_POINT('Ctrl Pts',(-10.0456553125043,0.819186572830302,
3.27862418762423));
#91750=CARTESIAN_POINT('Ctrl Pts',(-10.0626594394833,0.573692937217471,
3.2825081913052));
#91751=CARTESIAN_POINT('Ctrl Pts',(-10.0706621796009,0.327931798330226,
3.28639219498617));
#91752=CARTESIAN_POINT('Ctrl Pts',(-10.0742228583788,0.218584692361075,
3.28812031426496));
#91753=CARTESIAN_POINT('Ctrl Pts',(-10.0760022675563,0.109184672134251,
3.28984843354375));
#91754=CARTESIAN_POINT('Ctrl Pts',(-10.0759999978312,-0.000209059053492667,
3.29157655282254));
#91755=CARTESIAN_POINT('Ctrl Pts',(-10.0762484745384,-0.000209064208945703,
3.29157655282254));
#91756=CARTESIAN_POINT('Ctrl Pts',(-10.0765172050036,-0.290223858717575,
3.29615787373835));
#91757=CARTESIAN_POINT('Ctrl Pts',(-9.99523566685694,-2.20882270727419,
3.32646806444787));
#91758=CARTESIAN_POINT('Ctrl Pts',(-8.81522447115248,-5.66688708944764,
3.38250712495108));
#91759=CARTESIAN_POINT('Ctrl Pts',(-5.15686684570512,-9.12295875983689,
3.4596937343322));
#91760=CARTESIAN_POINT('Ctrl Pts',(-0.309172458345963,-10.4750423473345,
3.53688034371331));
#91761=CARTESIAN_POINT('Ctrl Pts',(3.64403776703417,-9.62007385115271,3.59891254985707));
#91762=CARTESIAN_POINT('Ctrl Pts',(5.60483013146509,-8.39954983073467,3.63521588620711));
#91763=CARTESIAN_POINT('Ctrl Pts',(6.13575050161833,-7.99155833647621,3.64579035276345));
#91764=CARTESIAN_POINT('',(-10.0752881866894,-8.86040407210159E-5,3.20842344717745));
#91765=CARTESIAN_POINT('Ctrl Pts',(-10.0752881866894,-8.86040407210159E-5,
3.20842344717745));
#91766=CARTESIAN_POINT('Ctrl Pts',(-10.0755181733502,-0.705362299928891,
3.21956149612057));
#91767=CARTESIAN_POINT('Ctrl Pts',(-9.83358734487156,-3.03966120371691,
3.25642841485739));
#91768=CARTESIAN_POINT('Ctrl Pts',(-8.04938962653146,-6.71037259617267,
3.31902420338792));
#91769=CARTESIAN_POINT('Ctrl Pts',(-3.99287690887074,-9.6891020991096,3.39621081276903));
#91770=CARTESIAN_POINT('Ctrl Pts',(0.984510208053555,-10.4332411960233,
3.47339742215015));
#91771=CARTESIAN_POINT('Ctrl Pts',(4.39868813687642,-9.23866752856937,3.52887331051089));
#91772=CARTESIAN_POINT('Ctrl Pts',(5.93475608800304,-8.14744207333764,3.55862032907792));
#91773=CARTESIAN_POINT('Ctrl Pts',(6.1363657837075,-7.99235873417456,3.56263847785126));
#91774=CARTESIAN_POINT('Ctrl Pts',(6.1362409016225,-7.9921963794308,2.56263886265602));
#91775=CARTESIAN_POINT('Ctrl Pts',(7.16828197515765,-7.19822956485664,2.58320748142331));
#91776=CARTESIAN_POINT('Ctrl Pts',(9.14580362631273,-4.9594312981428,2.6295049699843));
#91777=CARTESIAN_POINT('Ctrl Pts',(10.4697637918774,-0.453671087720179,
2.701531328339));
#91778=CARTESIAN_POINT('Ctrl Pts',(9.47394258585729,4.47952935166234,2.77871793772012));
#91779=CARTESIAN_POINT('Ctrl Pts',(6.29315192521423,8.37961873334699,2.85590454710123));
#91780=CARTESIAN_POINT('Ctrl Pts',(1.6609755745572,10.347121897175,2.93309115648235));
#91781=CARTESIAN_POINT('Ctrl Pts',(-3.35427053915678,9.92827478991659,3.01027776586346));
#91782=CARTESIAN_POINT('Ctrl Pts',(-7.59592332616536,7.21967591544794,3.08746437524457));
#91783=CARTESIAN_POINT('Ctrl Pts',(-9.72645285448307,3.47712916071539,3.15351293568257));
#91784=CARTESIAN_POINT('Ctrl Pts',(-10.0749869046441,0.923818464413679,
3.19383262632687));
#91785=CARTESIAN_POINT('Ctrl Pts',(-10.0752881866894,-8.86040407210159E-5,
3.20842344717745));
#91786=CARTESIAN_POINT('Origin',(0.,0.,-2.20842344717745));
#91787=CARTESIAN_POINT('',(6.13611323687281,-7.99203043615932,1.56263897033545));
#91788=CARTESIAN_POINT('',(6.13568652661064,-7.99147452837712,1.64578849738327));
#91789=CARTESIAN_POINT('',(6.13615379320824,-7.992083121821,-2.20842344717745));
#91790=CARTESIAN_POINT('',(-10.0759999984503,-0.000176720804854386,2.29157655282254));
#91791=CARTESIAN_POINT('Ctrl Pts',(6.13568652661064,-7.99147452837712,1.64578849738327));
#91792=CARTESIAN_POINT('Ctrl Pts',(6.78214643002692,-7.49513482539196,1.65865957111104));
#91793=CARTESIAN_POINT('Ctrl Pts',(8.54213696741524,-5.77384824740789,1.69725951463251));
#91794=CARTESIAN_POINT('Ctrl Pts',(10.2941112079739,-1.9629174193269,1.76158832794768));
#91795=CARTESIAN_POINT('Ctrl Pts',(10.022138899288,3.06243403856305,1.8387749373288));
#91796=CARTESIAN_POINT('Ctrl Pts',(7.43876696437783,7.38149824946882,1.91596154670991));
#91797=CARTESIAN_POINT('Ctrl Pts',(3.13979685689322,9.99817213565975,1.99314815609103));
#91798=CARTESIAN_POINT('Ctrl Pts',(-1.88330263600878,10.3089738354113,2.07033476547214));
#91799=CARTESIAN_POINT('Ctrl Pts',(-6.47205721978153,8.24222334685567,2.14752137485326));
#91800=CARTESIAN_POINT('Ctrl Pts',(-9.43020620361965,4.45136803055563,2.22126863579156));
#91801=CARTESIAN_POINT('Ctrl Pts',(-10.0752698966321,1.41075423147899,2.26928702693616));
#91802=CARTESIAN_POINT('Ctrl Pts',(-10.0764446330389,-0.000176441506157512,
2.29157654828705));
#91803=CARTESIAN_POINT('Ctrl Pts',(-10.0759999984503,-0.000176720804854386,
2.29157655282254));
#91804=CARTESIAN_POINT('Ctrl Pts',(-10.0759961802274,-0.217878384328413,
2.29501589975352));
#91805=CARTESIAN_POINT('Ctrl Pts',(-10.068934916524,-0.435554421608969,
2.2984552466845));
#91806=CARTESIAN_POINT('Ctrl Pts',(-10.0548329534,-0.652771230387034,2.30189459361548));
#91807=CARTESIAN_POINT('Ctrl Pts',(-10.0388453706317,-0.899032809606319,
2.30579382688141));
#91808=CARTESIAN_POINT('Ctrl Pts',(-10.0138040511016,-1.14474211387924,
2.30969306014734));
#91809=CARTESIAN_POINT('Ctrl Pts',(-9.97977104745379,-1.3892249063428,2.31359229341327));
#91810=CARTESIAN_POINT('Ctrl Pts',(-9.94574361994677,-1.63366764149921,
2.31749088780894));
#91811=CARTESIAN_POINT('Ctrl Pts',(-9.90272748779683,-1.87688399017187,
2.32138948220462));
#91812=CARTESIAN_POINT('Ctrl Pts',(-9.85083638520011,-2.1182064375357,2.32528807660029));
#91813=CARTESIAN_POINT('Ctrl Pts',(-9.79895057382811,-2.35950427776585,
2.32918627346463));
#91814=CARTESIAN_POINT('Ctrl Pts',(-9.73819165759179,-2.59890832998929,
2.33308447032897));
#91815=CARTESIAN_POINT('Ctrl Pts',(-9.66872437485874,-2.83576179588704,
2.33698266719331));
#91816=CARTESIAN_POINT('Ctrl Pts',(-9.59925191932735,-3.07263289879557,
2.34088115433223));
#91817=CARTESIAN_POINT('Ctrl Pts',(-9.52106987730694,-3.30695276769737,
2.34477964147116));
#91818=CARTESIAN_POINT('Ctrl Pts',(-9.43439307949502,-3.53807902986585,
2.34867812861008));
#91819=CARTESIAN_POINT('Ctrl Pts',(-9.3477172398397,-3.76920273708122,2.35257657265371));
#91820=CARTESIAN_POINT('Ctrl Pts',(-9.25254693202794,-3.99713264800795,
2.35647501669735));
#91821=CARTESIAN_POINT('Ctrl Pts',(-9.14914570445701,-4.22124494416231,
2.36037346074099));
#91822=CARTESIAN_POINT('Ctrl Pts',(-9.0457237758488,-4.44540210784007,2.36427268525732));
#91823=CARTESIAN_POINT('Ctrl Pts',(-8.93406775112007,-4.66573987626492,
2.36817190977366));
#91824=CARTESIAN_POINT('Ctrl Pts',(-8.81448843710067,-4.88165643938803,
2.37207113429));
#91825=CARTESIAN_POINT('Ctrl Pts',(-8.74282810193653,-5.01104882976736,
2.37440782385887));
#91826=CARTESIAN_POINT('Ctrl Pts',(-8.66832321219159,-5.13885390250795,
2.37674451342773));
#91827=CARTESIAN_POINT('Ctrl Pts',(-8.59104846906926,-5.26494655263496,
2.3790812029966));
#91828=CARTESIAN_POINT('Ctrl Pts',(-8.46210012681553,-5.47535732266519,
2.38298043622717));
#91829=CARTESIAN_POINT('Ctrl Pts',(-8.32539954109015,-5.68105875354989,
2.38687966945774));
#91830=CARTESIAN_POINT('Ctrl Pts',(-8.18131593054936,-5.88148328608857,
2.39077890268831));
#91831=CARTESIAN_POINT('Ctrl Pts',(-8.03725592740549,-6.08187498004505,
2.39467749704854));
#91832=CARTESIAN_POINT('Ctrl Pts',(-7.88581547691877,-6.27699127552694,
2.39857609140876));
#91833=CARTESIAN_POINT('Ctrl Pts',(-7.72740638591762,-6.46629465357709,
2.40247468576899));
#91834=CARTESIAN_POINT('Ctrl Pts',(-7.56901344755157,-6.65557872876796,
2.40637288259791));
#91835=CARTESIAN_POINT('Ctrl Pts',(-7.40365346630422,-6.83905085647716,
2.41027107942683));
#91836=CARTESIAN_POINT('Ctrl Pts',(-7.2317783757314,-7.01620677605099,2.41416927625576));
#91837=CARTESIAN_POINT('Ctrl Pts',(-7.05989048667257,-7.19337588734183,
2.41806776335954));
#91838=CARTESIAN_POINT('Ctrl Pts',(-6.88148671091967,-7.3642276487559,2.42196625046332));
#91839=CARTESIAN_POINT('Ctrl Pts',(-6.69705657292911,-7.52829391422698,
2.4258647375671));
#91840=CARTESIAN_POINT('Ctrl Pts',(-6.5126284736855,-7.69235836605957,2.42976318157582));
#91841=CARTESIAN_POINT('Ctrl Pts',(-6.32217435503862,-7.84963728834382,
2.43366162558454));
#91842=CARTESIAN_POINT('Ctrl Pts',(-6.12621819150001,-7.99970166132052,
2.43756006959325));
#91843=CARTESIAN_POINT('Ctrl Pts',(-5.93022279729805,-8.14979607736804,
2.44145929407522));
#91844=CARTESIAN_POINT('Ctrl Pts',(-5.72872337816251,-8.29267288815728,
2.44535851855719));
#91845=CARTESIAN_POINT('Ctrl Pts',(-5.52227545736255,-8.4279445758151,2.44925774303916));
#91846=CARTESIAN_POINT('Ctrl Pts',(-5.39855733116427,-8.50900889295551,
2.45159443281868));
#91847=CARTESIAN_POINT('Ctrl Pts',(-5.27306265851896,-8.58734283382268,
2.4539311225982));
#91848=CARTESIAN_POINT('Ctrl Pts',(-5.14591584904406,-8.66287054471883,
2.45626781237772));
#91849=CARTESIAN_POINT('Ctrl Pts',(-4.93374602039322,-8.78890360481217,
2.46016704565127));
#91850=CARTESIAN_POINT('Ctrl Pts',(-4.71691333637528,-8.90715637330441,
2.46406627892482));
#91851=CARTESIAN_POINT('Ctrl Pts',(-4.49600902900801,-9.01729886446481,
2.46796551219837));
#91852=CARTESIAN_POINT('Ctrl Pts',(-4.27514091573067,-9.12742330931694,
2.47186410660163));
#91853=CARTESIAN_POINT('Ctrl Pts',(-4.05020276013291,-9.22944000533982,
2.47576270100488));
#91854=CARTESIAN_POINT('Ctrl Pts',(-3.82180946694097,-9.32306539708912,
2.47966129540814));
#91855=CARTESIAN_POINT('Ctrl Pts',(-3.59343946252863,-9.41668124205582,
2.48355949228));
#91856=CARTESIAN_POINT('Ctrl Pts',(-3.36161528174511,-9.50190738564849,
2.48745768915185));
#91857=CARTESIAN_POINT('Ctrl Pts',(-3.12697182419795,-9.57850840218205,
2.49135588602371));
#91858=CARTESIAN_POINT('Ctrl Pts',(-2.89231089421434,-9.65511512271608,
2.49525437317));
#91859=CARTESIAN_POINT('Ctrl Pts',(-2.65483053200803,-9.72309534371056,
2.49915286031629));
#91860=CARTESIAN_POINT('Ctrl Pts',(-2.41518205709183,-9.78226311397836,
2.50305134746258));
#91861=CARTESIAN_POINT('Ctrl Pts',(-2.17553623134171,-9.84143023018295,
2.5069497915135));
#91862=CARTESIAN_POINT('Ctrl Pts',(-1.93372261184902,-9.89178502575761,
2.51084823556442));
#91863=CARTESIAN_POINT('Ctrl Pts',(-1.69040475534258,-9.93319222421046,
2.51474667961534));
#91864=CARTESIAN_POINT('Ctrl Pts',(-1.44703818635148,-9.97460771242696,
2.51864590413877));
#91865=CARTESIAN_POINT('Ctrl Pts',(-1.20216705328294,-10.0070719768972,
2.52254512866219));
#91866=CARTESIAN_POINT('Ctrl Pts',(-0.956463475878432,-10.0305011649125,
2.52644435318561));
#91867=CARTESIAN_POINT('Ctrl Pts',(-0.809220614642379,-10.0445415818907,
2.52878104271002));
#91868=CARTESIAN_POINT('Ctrl Pts',(-0.661678939472876,-10.0553382699226,
2.53111773223442));
#91869=CARTESIAN_POINT('Ctrl Pts',(-0.513983875818206,-10.0628821207147,
2.53345442175883));
#91870=CARTESIAN_POINT('Ctrl Pts',(-0.267525157741719,-10.0754705427618,
2.5373536550201));
#91871=CARTESIAN_POINT('Ctrl Pts',(-0.0205683639859459,-10.0790020847021,
2.54125288828137));
#91872=CARTESIAN_POINT('Ctrl Pts',(0.226209615553745,-10.0734604386889,
2.54515212154265));
#91873=CARTESIAN_POINT('Ctrl Pts',(0.472947161739886,-10.0679197006471,
2.5490507159338));
#91874=CARTESIAN_POINT('Ctrl Pts',(0.719505673756191,-10.0533087486379,
2.55294931032495));
#91875=CARTESIAN_POINT('Ctrl Pts',(0.965208964084447,-10.0296633869563,
2.55684790471611));
#91876=CARTESIAN_POINT('Ctrl Pts',(1.21088720058246,-10.0060204363407,2.56074610157607));
#91877=CARTESIAN_POINT('Ctrl Pts',(1.45571011226613,-9.9733449422247,2.56464429843603));
#91878=CARTESIAN_POINT('Ctrl Pts',(1.6990062599891,-9.93172460998179,2.56854249529599));
#91879=CARTESIAN_POINT('Ctrl Pts',(1.94232052448544,-9.89010117852775,2.57244098243079));
#91880=CARTESIAN_POINT('Ctrl Pts',(2.18410752271826,-9.83953162225846,2.57633946956558));
#91881=CARTESIAN_POINT('Ctrl Pts',(2.42370435354384,-9.78015507068332,2.58023795670038));
#91882=CARTESIAN_POINT('Ctrl Pts',(2.66329853578938,-9.72077917547558,2.58413640074005));
#91883=CARTESIAN_POINT('Ctrl Pts',(2.90070232909134,-9.65259654875453,2.58803484477972));
#91884=CARTESIAN_POINT('Ctrl Pts',(3.13526563019086,-9.57579685603992,2.59193328881939));
#91885=CARTESIAN_POINT('Ctrl Pts',(3.36987589113122,-9.49898178793909,2.59583251333202));
#91886=CARTESIAN_POINT('Ctrl Pts',(3.60164425852563,-9.41354629294794,2.59973173784464));
#91887=CARTESIAN_POINT('Ctrl Pts',(3.82993702673016,-9.3197295224315,2.60363096235726));
#91888=CARTESIAN_POINT('Ctrl Pts',(3.96674611124785,-9.26350791459125,2.60596765195149));
#91889=CARTESIAN_POINT('Ctrl Pts',(4.10230736223007,-9.20427732353835,2.60830434154571));
#91890=CARTESIAN_POINT('Ctrl Pts',(4.2364878777232,-9.14209748700507,2.61064103113994));
#91891=CARTESIAN_POINT('Ctrl Pts',(4.46039355290455,-9.03833861985149,2.61454024153842));
#91892=CARTESIAN_POINT('Ctrl Pts',(4.68051769765676,-8.92633516334218,2.6184394519369));
#91893=CARTESIAN_POINT('Ctrl Pts',(4.89625388547097,-8.80638824314545,2.62233866233539));
#91894=CARTESIAN_POINT('Ctrl Pts',(5.11249823727535,-8.68615878942389,2.62624705727697));
#91895=CARTESIAN_POINT('Ctrl Pts',(5.32433367772899,-8.55794851900752,2.63015545221855));
#91896=CARTESIAN_POINT('Ctrl Pts',(5.53117432236376,-8.42210701758318,2.63406384716013));
#91897=CARTESIAN_POINT('Ctrl Pts',(5.73801496699853,-8.28626551615884,2.63797224210171));
#91898=CARTESIAN_POINT('Ctrl Pts',(5.93986057789858,-8.14279293543828,2.64188063704329));
#91899=CARTESIAN_POINT('Ctrl Pts',(6.13615379320825,-7.99208312182099,2.64578903198487));
#91900=CARTESIAN_POINT('',(-10.0753832650889,-0.000140516250313333,2.20842344717745));
#91901=CARTESIAN_POINT('Ctrl Pts',(-10.0753832650889,-0.000140516250313333,
2.20842344717745));
#91902=CARTESIAN_POINT('Ctrl Pts',(-10.0757149532685,-0.63308601055591,
2.21841952213574));
#91903=CARTESIAN_POINT('Ctrl Pts',(-9.86563371722133,-2.89495068052824,
2.25414446688773));
#91904=CARTESIAN_POINT('Ctrl Pts',(-8.19195912274756,-6.53556248896653,
2.31559828143343));
#91905=CARTESIAN_POINT('Ctrl Pts',(-4.20050058358688,-9.60091486080197,
2.39278489081454));
#91906=CARTESIAN_POINT('Ctrl Pts',(0.759716778100874,-10.4520142428044,
2.46997150019566));
#91907=CARTESIAN_POINT('Ctrl Pts',(4.26961744480485,-9.30813086285984,2.52658949080948));
#91908=CARTESIAN_POINT('Ctrl Pts',(5.87732264030094,-8.1913866175406,2.5574786116296));
#91909=CARTESIAN_POINT('Ctrl Pts',(6.1362409016225,-7.9921963794308,2.56263886265602));
#91910=CARTESIAN_POINT('Ctrl Pts',(6.13611323687281,-7.99203043615932,1.56263897033545));
#91911=CARTESIAN_POINT('Ctrl Pts',(7.1109225332917,-7.24211522249615,1.58206557922476));
#91912=CARTESIAN_POINT('Ctrl Pts',(9.05946263688066,-5.08416455109786,1.62722105790779));
#91913=CARTESIAN_POINT('Ctrl Pts',(10.4575734376389,-0.678917602467889,
1.69810540638452));
#91914=CARTESIAN_POINT('Ctrl Pts',(9.56816533664898,4.27457406171102,1.77529201576563));
#91915=CARTESIAN_POINT('Ctrl Pts',(6.47205724804309,8.24222338284801,1.85247862514674));
#91916=CARTESIAN_POINT('Ctrl Pts',(1.8833026442324,10.3089738804262,1.92966523452786));
#91917=CARTESIAN_POINT('Ctrl Pts',(-3.1397968706035,9.99817217931868,2.00685184390897));
#91918=CARTESIAN_POINT('Ctrl Pts',(-7.43876699686031,7.38149828170111,2.08403845329009));
#91919=CARTESIAN_POINT('Ctrl Pts',(-9.6875785856742,3.62177575817932,2.15122898771292));
#91920=CARTESIAN_POINT('Ctrl Pts',(-10.074861221977,0.996050653330273,2.19269065234204));
#91921=CARTESIAN_POINT('Ctrl Pts',(-10.0753832650889,-0.000140516250313333,
2.20842344717745));
#91922=CARTESIAN_POINT('Origin',(0.,0.,-2.20842344717745));
#91923=CARTESIAN_POINT('',(6.13615379320823,-7.99208312182101,0.562637467686473));
#91924=CARTESIAN_POINT('',(6.13570130489945,-7.99149349283587,0.645787560180936));
#91925=CARTESIAN_POINT('',(6.13615379320824,-7.992083121821,-2.20842344717745));
#91926=CARTESIAN_POINT('',(-10.0759532185556,-0.00022630263218971,0.208423447557889));
#91927=CARTESIAN_POINT('Ctrl Pts',(-10.0759999974585,-0.000226308042700162,
0.208423447626752));
#91928=CARTESIAN_POINT('Ctrl Pts',(-10.0759942294301,-0.25703845579838,
0.212479650651435));
#91929=CARTESIAN_POINT('Ctrl Pts',(-10.0661658676225,-0.513807198917835,
0.216535853676117));
#91930=CARTESIAN_POINT('Ctrl Pts',(-10.0465508416353,-0.769800095114306,
0.220592056700798));
#91931=CARTESIAN_POINT('Ctrl Pts',(-10.0288714897423,-1.00053078580477,
0.224247980514977));
#91932=CARTESIAN_POINT('Ctrl Pts',(-10.0032424030593,-1.23063110424319,
0.227903904329156));
#91933=CARTESIAN_POINT('Ctrl Pts',(-9.96972602448593,-1.45956808566372,
0.231559828143335));
#91934=CARTESIAN_POINT('Ctrl Pts',(-9.93400236370396,-1.70358212932921,
0.235456519484748));
#91935=CARTESIAN_POINT('Ctrl Pts',(-9.88931045279285,-1.94632091839481,
0.239353210826162));
#91936=CARTESIAN_POINT('Ctrl Pts',(-9.83576585870345,-2.18711818902491,
0.243249902167575));
#91937=CARTESIAN_POINT('Ctrl Pts',(-9.78223042362828,-2.42787427033115,
0.24714592696455));
#91938=CARTESIAN_POINT('Ctrl Pts',(-9.71984538890546,-2.66668922356591,
0.251041951761524));
#91939=CARTESIAN_POINT('Ctrl Pts',(-9.64877730110775,-2.90290761024662,
0.254937976558499));
#91940=CARTESIAN_POINT('Ctrl Pts',(-9.57771682973085,-3.13910068122392,
0.258833583815545));
#91941=CARTESIAN_POINT('Ctrl Pts',(-9.49797524383153,-3.37269747383736,
0.262729191072592));
#91942=CARTESIAN_POINT('Ctrl Pts',(-9.40976907379589,-3.6030573098182,0.266624798329638));
#91943=CARTESIAN_POINT('Ctrl Pts',(-9.32155660289302,-3.83343360118696,
0.270520683863183));
#91944=CARTESIAN_POINT('Ctrl Pts',(-9.22487843689419,-4.06057221193792,
0.274416569396729));
#91945=CARTESIAN_POINT('Ctrl Pts',(-9.11999988210158,-4.28385085530149,
0.278312454930274));
#91946=CARTESIAN_POINT('Ctrl Pts',(-9.01512255625489,-4.50712688233057,
0.282208294812612));
#91947=CARTESIAN_POINT('Ctrl Pts',(-8.90204515448193,-4.72654278042739,
0.286104134694949));
#91948=CARTESIAN_POINT('Ctrl Pts',(-8.78108005545656,-4.94149866535073,
0.289999974577287));
#91949=CARTESIAN_POINT('Ctrl Pts',(-8.66009032665029,-5.15649831757879,
0.293896607694066));
#91950=CARTESIAN_POINT('Ctrl Pts',(-8.53120982810265,-5.36703589826419,
0.297793240810845));
#91951=CARTESIAN_POINT('Ctrl Pts',(-8.39479627757849,-5.57253725496333,
0.301689873927624));
#91952=CARTESIAN_POINT('Ctrl Pts',(-8.31245075295972,-5.69658737287492,
0.304042061793237));
#91953=CARTESIAN_POINT('Ctrl Pts',(-8.22736113194365,-5.81880286809109,
0.30639424965885));
#91954=CARTESIAN_POINT('Ctrl Pts',(-8.13961371352563,-5.93906260234605,
0.308746437524462));
#91955=CARTESIAN_POINT('Ctrl Pts',(-7.99412393307036,-6.1384594923037,0.312646487261849));
#91956=CARTESIAN_POINT('Ctrl Pts',(-7.84128311980634,-6.33253588031595,
0.316546536999235));
#91957=CARTESIAN_POINT('Ctrl Pts',(-7.6815052180949,-6.520755599191,0.320446586736622));
#91958=CARTESIAN_POINT('Ctrl Pts',(-7.52175316747803,-6.70894486525812,
0.324346005469636));
#91959=CARTESIAN_POINT('Ctrl Pts',(-7.35506644915583,-6.89127914173186,
0.328245424202651));
#91960=CARTESIAN_POINT('Ctrl Pts',(-7.18189903465007,-7.06725563822991,
0.332144842935665));
#91961=CARTESIAN_POINT('Ctrl Pts',(-7.0087490348349,-7.24321443754025,0.336043869521167));
#91962=CARTESIAN_POINT('Ctrl Pts',(-6.82911983543161,-7.41281653523007,
0.339942896106669));
#91963=CARTESIAN_POINT('Ctrl Pts',(-6.64350272377713,-7.57559552505054,
0.343841922692171));
#91964=CARTESIAN_POINT('Ctrl Pts',(-6.45787168682691,-7.73838672681394,
0.34774124178895));
#91965=CARTESIAN_POINT('Ctrl Pts',(-6.26625204748849,-7.89435361222738,
0.351640560885729));
#91966=CARTESIAN_POINT('Ctrl Pts',(-6.06916965264334,-8.04306880036675,
0.355539879982508));
#91967=CARTESIAN_POINT('Ctrl Pts',(-5.87208944175096,-8.19178234053068,
0.359439155869295));
#91968=CARTESIAN_POINT('Ctrl Pts',(-5.66954681992957,-8.33324417813178,
0.363338431756081));
#91969=CARTESIAN_POINT('Ctrl Pts',(-5.46209882225758,-8.46706870504146,
0.367237707642868));
#91970=CARTESIAN_POINT('Ctrl Pts',(-5.25460959742125,-8.60091982755979,
0.371137758451995));
#91971=CARTESIAN_POINT('Ctrl Pts',(-5.04221328251075,-8.72713045517242,
0.375037809261121));
#91972=CARTESIAN_POINT('Ctrl Pts',(-4.82549501839948,-8.84535888629748,
0.378937860070248));
#91973=CARTESIAN_POINT('Ctrl Pts',(-4.69592536044032,-8.91604428720148,
0.381269589015356));
#91974=CARTESIAN_POINT('Ctrl Pts',(-4.56481133630743,-8.98387730628482,
0.383601317960464));
#91975=CARTESIAN_POINT('Ctrl Pts',(-4.43228219470303,-9.04879276735402,
0.385933046905572));
#91976=CARTESIAN_POINT('Ctrl Pts',(-4.21066501416261,-9.15734535647877,
0.38983219835516));
#91977=CARTESIAN_POINT('Ctrl Pts',(-3.98502618871533,-9.25776808083673,
0.393731349804748));
#91978=CARTESIAN_POINT('Ctrl Pts',(-3.75598155591525,-9.34977959909347,
0.397630501254335));
#91979=CARTESIAN_POINT('Ctrl Pts',(-3.52697444811622,-9.44177604285457,
0.401529013895406));
#91980=CARTESIAN_POINT('Ctrl Pts',(-3.29456290534006,-9.52536392768369,
0.405427526536476));
#91981=CARTESIAN_POINT('Ctrl Pts',(-3.05938262588567,-9.60031009647235,
0.409326039177547));
#91982=CARTESIAN_POINT('Ctrl Pts',(-2.8242263093315,-9.67524862887428,0.413224154592839));
#91983=CARTESIAN_POINT('Ctrl Pts',(-2.58630208482971,-9.74154711887444,
0.417122270008131));
#91984=CARTESIAN_POINT('Ctrl Pts',(-2.34626170857426,-9.79902199175398,
0.421020385423424));
#91985=CARTESIAN_POINT('Ctrl Pts',(-2.10620339325966,-9.85650115993235,
0.424918792158552));
#91986=CARTESIAN_POINT('Ctrl Pts',(-1.8640288805491,-9.9051553257431,0.42881719889368));
#91987=CARTESIAN_POINT('Ctrl Pts',(-1.62040231297615,-9.94485154962615,
0.432715605628809));
#91988=CARTESIAN_POINT('Ctrl Pts',(-1.37677839311814,-9.98454734209366,
0.43661396999635));
#91989=CARTESIAN_POINT('Ctrl Pts',(-1.13170272534691,-10.0152853446242,
0.440512334363892));
#91990=CARTESIAN_POINT('Ctrl Pts',(-0.885847572329198,-10.0369841127003,
0.444410698731434));
#91991=CARTESIAN_POINT('Ctrl Pts',(-0.639943094035444,-10.0586872341435,
0.448309845217618));
#91992=CARTESIAN_POINT('Ctrl Pts',(-0.393259095630425,-10.0713474723984,
0.452208991703801));
#91993=CARTESIAN_POINT('Ctrl Pts',(-0.146472237457178,-10.0749353290061,
0.456108138189985));
#91994=CARTESIAN_POINT('Ctrl Pts',(0.00145334302901629,-10.0770859126121,
0.458445310888883));
#91995=CARTESIAN_POINT('Ctrl Pts',(0.149415822465978,-10.0759779000816,
0.460782483587781));
#91996=CARTESIAN_POINT('Ctrl Pts',(0.297269420956911,-10.0716139169134,
0.46311965628668));
#91997=CARTESIAN_POINT('Ctrl Pts',(0.543933112644408,-10.0643334975681,
0.467018754123361));
#91998=CARTESIAN_POINT('Ctrl Pts',(0.790364757584853,-10.0479861342427,
0.470917851960043));
#91999=CARTESIAN_POINT('Ctrl Pts',(1.03588839359109,-10.0226100011935,0.474816949796724));
#92000=CARTESIAN_POINT('Ctrl Pts',(1.28137167075645,-9.99723803943839,0.478715406705014));
#92001=CARTESIAN_POINT('Ctrl Pts',(1.52594695987715,-9.96284029941278,0.482613863613304));
#92002=CARTESIAN_POINT('Ctrl Pts',(1.76894318917324,-9.91950684225167,0.486512320521594));
#92003=CARTESIAN_POINT('Ctrl Pts',(2.01191453732034,-9.87617782213967,0.490410378254607));
#92004=CARTESIAN_POINT('Ctrl Pts',(2.25330687424229,-9.82391496077854,0.49430843598762));
#92005=CARTESIAN_POINT('Ctrl Pts',(2.49245803488221,-9.76285967042193,0.498206493720633));
#92006=CARTESIAN_POINT('Ctrl Pts',(2.73162691207991,-9.7017998570282,0.502104840225671));
#92007=CARTESIAN_POINT('Ctrl Pts',(2.96855401051834,-9.6319463793504,0.506003186730709));
#92008=CARTESIAN_POINT('Ctrl Pts',(3.20258981139837,-9.55349122048727,0.509901533235747));
#92009=CARTESIAN_POINT('Ctrl Pts',(3.43662298778403,-9.47503694142596,0.513799836024446));
#92010=CARTESIAN_POINT('Ctrl Pts',(3.6677646678912,-9.38798126467973,0.517698138813145));
#92011=CARTESIAN_POINT('Ctrl Pts',(3.89538215396801,-9.2925655162903,0.521596441601844));
#92012=CARTESIAN_POINT('Ctrl Pts',(4.12304520773466,-9.19713066622593,0.525495524807968));
#92013=CARTESIAN_POINT('Ctrl Pts',(4.34718240042929,-9.09333250760053,0.529394608014092));
#92014=CARTESIAN_POINT('Ctrl Pts',(4.56718135925702,-8.98146037299365,0.533293691220216));
#92015=CARTESIAN_POINT('Ctrl Pts',(4.69907211370827,-8.91439232724472,0.535631216036079));
#92016=CARTESIAN_POINT('Ctrl Pts',(4.82947597035662,-8.8444233435605,0.537968740851943));
#92017=CARTESIAN_POINT('Ctrl Pts',(4.95826512212948,-8.77162373672483,0.540306265667806));
#92018=CARTESIAN_POINT('Ctrl Pts',(5.17310996842347,-8.65018012035209,0.544205702482626));
#92019=CARTESIAN_POINT('Ctrl Pts',(5.38352161164181,-8.52082199850081,0.548105139297447));
#92020=CARTESIAN_POINT('Ctrl Pts',(5.58891975052209,-8.38389837857211,0.552004576112267));
#92021=CARTESIAN_POINT('Ctrl Pts',(5.77561133736504,-8.25944502169106,0.55554887330367));
#92022=CARTESIAN_POINT('Ctrl Pts',(5.9581612082682,-8.12874209528196,0.559093170495071));
#92023=CARTESIAN_POINT('Ctrl Pts',(6.13615379320823,-7.99208312182101,0.562637467686473));
#92024=CARTESIAN_POINT('',(-2.60234962446759,9.73414364143212,0.));
#92025=CARTESIAN_POINT('Ctrl Pts',(-2.60234962446759,9.73414364143212,0.));
#92026=CARTESIAN_POINT('Ctrl Pts',(-4.17596404974509,9.31344973557609,0.0257288697937048));
#92027=CARTESIAN_POINT('Ctrl Pts',(-7.11402029978251,7.69532831508128,0.0771866093811144));
#92028=CARTESIAN_POINT('Ctrl Pts',(-9.60465795441405,3.91079428092824,0.146661091773599));
#92029=CARTESIAN_POINT('Ctrl Pts',(-10.0747624470573,1.14044107610686,0.190406704372379));
#92030=CARTESIAN_POINT('Ctrl Pts',(-10.0756947894608,-0.000226272741935124,
0.208423447177455));
#92031=CARTESIAN_POINT('',(2.60261129514636,9.73435190842889,-4.86806775445991E-16));
#92032=CARTESIAN_POINT('Origin',(0.,0.,0.));
#92033=CARTESIAN_POINT('',(-10.0767271183091,-6.71673636424164E-5,0.291576552822545));
#92034=CARTESIAN_POINT('Ctrl Pts',(2.60261129514636,9.73435190842889,-4.86806775445991E-16));
#92035=CARTESIAN_POINT('Ctrl Pts',(1.30817124105572,10.0791274528727,0.0211609738543883));
#92036=CARTESIAN_POINT('Ctrl Pts',(-1.71444551568512,10.2699371933317,0.0680508175024821));
#92037=CARTESIAN_POINT('Ctrl Pts',(-6.11133505897136,8.51314768957044,0.14066953094428));
#92038=CARTESIAN_POINT('Ctrl Pts',(-9.32646956261626,4.73974294579722,0.216700741364073));
#92039=CARTESIAN_POINT('Ctrl Pts',(-10.0761339447278,1.55531013884913,0.267003081990161));
#92040=CARTESIAN_POINT('Ctrl Pts',(-10.0767271183091,-6.71673636424164E-5,
0.291576552822545));
#92041=CARTESIAN_POINT('Ctrl Pts',(-10.0767271183091,-6.71673636424164E-5,
0.291576552822545));
#92042=CARTESIAN_POINT('Ctrl Pts',(-10.0767550082293,-0.0731981196951006,
0.292731951783866));
#92043=CARTESIAN_POINT('Ctrl Pts',(-10.0585961450043,-1.7748235789123,0.319616220538893));
#92044=CARTESIAN_POINT('Ctrl Pts',(-9.16254767717503,-5.08620698909665,
0.372229359087624));
#92045=CARTESIAN_POINT('Ctrl Pts',(-5.73484093405497,-8.77116607832706,
0.449415968468739));
#92046=CARTESIAN_POINT('Ctrl Pts',(-0.984510201175506,-10.4332411554452,
0.526602577849852));
#92047=CARTESIAN_POINT('Ctrl Pts',(3.2365044433575,-9.80218273326553,0.592059775087324));
#92048=CARTESIAN_POINT('Ctrl Pts',(5.43245140071271,-8.53118528820037,0.631788102531087));
#92049=CARTESIAN_POINT('Ctrl Pts',(6.13570130491008,-7.99149349282772,0.645787560181147));
#92050=CARTESIAN_POINT('Origin',(0.,0.,0.));
#92051=CARTESIAN_POINT('',(-9.51749999795141,-0.000197471173248046,3.61402667816495));
#92052=CARTESIAN_POINT('',(-9.51745740801614,-0.000133057486098593,3.88597332183505));
#92053=CARTESIAN_POINT('',(-9.5175,-1.16555759108849E-15,0.));
#92054=CARTESIAN_POINT('',(-7.17753992463813,-6.25025814508694,4.));
#92055=CARTESIAN_POINT('Ctrl Pts',(-9.5174999990699,-0.000133058081536771,
3.88597332183505));
#92056=CARTESIAN_POINT('Ctrl Pts',(-9.51749665273006,-0.239493111281163,
3.8899746778871));
#92057=CARTESIAN_POINT('Ctrl Pts',(-9.50845929853709,-0.478827423920704,
3.89397603393915));
#92058=CARTESIAN_POINT('Ctrl Pts',(-9.49041975691978,-0.717453195314301,
3.8979773899912));
#92059=CARTESIAN_POINT('Ctrl Pts',(-9.47175816398719,-0.964307417192166,
3.90211672342915));
#92060=CARTESIAN_POINT('Ctrl Pts',(-9.44346254832326,-1.21040305961421,
3.9062560568671));
#92061=CARTESIAN_POINT('Ctrl Pts',(-9.40562656251792,-1.45498976506963,
3.91039539030505));
#92062=CARTESIAN_POINT('Ctrl Pts',(-9.36779057671258,-1.69957647052505,
3.91453472374299));
#92063=CARTESIAN_POINT('Ctrl Pts',(-9.32041427950108,-1.94265392739488,
3.91867405718094));
#92064=CARTESIAN_POINT('Ctrl Pts',(-9.26365005209081,-2.1834820728364,3.92281339061889));
#92065=CARTESIAN_POINT('Ctrl Pts',(-9.20909822162236,-2.41492389388337,
3.92679139272094));
#92066=CARTESIAN_POINT('Ctrl Pts',(-9.14586184258494,-2.64434941741664,
3.93076939482299));
#92067=CARTESIAN_POINT('Ctrl Pts',(-9.07411450088742,-2.87110645479834,
3.93474739692504));
#92068=CARTESIAN_POINT('Ctrl Pts',(-9.00237951233866,-3.09782445012847,
3.93872471411179));
#92069=CARTESIAN_POINT('Ctrl Pts',(-8.92213657000647,-3.32187461370113,
3.94270203129855));
#92070=CARTESIAN_POINT('Ctrl Pts',(-8.83360907565096,-3.54262006833601,
3.9466793484853));
#92071=CARTESIAN_POINT('Ctrl Pts',(-8.74509286899693,-3.76333737681344,
3.95065615854408));
#92072=CARTESIAN_POINT('Ctrl Pts',(-8.64829432222514,-3.98075056177624,
3.95463296860285));
#92073=CARTESIAN_POINT('Ctrl Pts',(-8.54348531568343,-4.19424187556007,
3.95860977866163));
#92074=CARTESIAN_POINT('Ctrl Pts',(-8.43867709176879,-4.40773159516714,
3.96258655902487));
#92075=CARTESIAN_POINT('Ctrl Pts',(-8.32585864693373,-4.6172992533984,3.96656333938812));
#92076=CARTESIAN_POINT('Ctrl Pts',(-8.205348783061,-4.82234980049347,3.97054011975136));
#92077=CARTESIAN_POINT('Ctrl Pts',(-8.08484685271647,-5.02738684849189,
3.97451663831115));
#92078=CARTESIAN_POINT('Ctrl Pts',(-7.95665465562245,-5.22790714217913,
3.97849315687094));
#92079=CARTESIAN_POINT('Ctrl Pts',(-7.82113590955983,-5.42334208161294,
3.98246967543072));
#92080=CARTESIAN_POINT('Ctrl Pts',(-7.68560746080289,-5.61879101354249,
3.98644647869609));
#92081=CARTESIAN_POINT('Ctrl Pts',(-7.54275157160334,-5.80915363661822,
3.99042328196147));
#92082=CARTESIAN_POINT('Ctrl Pts',(-7.3929747953963,-5.99389105044754,3.99440008522684));
#92083=CARTESIAN_POINT('Ctrl Pts',(-7.32267233336095,-6.08060339231482,
3.99626672348456));
#92084=CARTESIAN_POINT('Ctrl Pts',(-7.25084566524277,-6.16607684126215,
3.99813336174228));
#92085=CARTESIAN_POINT('Ctrl Pts',(-7.17753992463813,-6.25025814508694,
4.));
#92086=CARTESIAN_POINT('',(7.17753995915506,-6.25025810544912,3.99999685725335));
#92087=CARTESIAN_POINT('Origin',(0.,0.,4.));
#92088=CARTESIAN_POINT('Ctrl Pts',(7.17753995915506,-6.25025810544912,3.99999685725336));
#92089=CARTESIAN_POINT('Ctrl Pts',(7.02281523419272,-6.42793763121434,3.99605653063733));
#92090=CARTESIAN_POINT('Ctrl Pts',(6.86146956740091,-6.59989196979162,3.9921162040213));
#92091=CARTESIAN_POINT('Ctrl Pts',(6.69395260357331,-6.76563410118476,3.98817587740527));
#92092=CARTESIAN_POINT('Ctrl Pts',(6.52645659093536,-6.93135550336488,3.9842360436022));
#92093=CARTESIAN_POINT('Ctrl Pts',(6.35279102598433,-7.09086604782969,3.98029620979912));
#92094=CARTESIAN_POINT('Ctrl Pts',(6.17344244262228,-7.24371552848605,3.97635637599605));
#92095=CARTESIAN_POINT('Ctrl Pts',(5.99408383571268,-7.39657355169127,3.97241632200104));
#92096=CARTESIAN_POINT('Ctrl Pts',(5.80904179231516,-7.54276957913585,3.96847626800604));
#92097=CARTESIAN_POINT('Ctrl Pts',(5.61883685492493,-7.68189290785399,3.96453621401103));
#92098=CARTESIAN_POINT('Ctrl Pts',(5.4286329598901,-7.82101547415262,3.96059618160819));
#92099=CARTESIAN_POINT('Ctrl Pts',(5.23326646037713,-7.95306525185556,3.95665614920535));
#92100=CARTESIAN_POINT('Ctrl Pts',(5.03328843794528,-8.07767378336402,3.95271611680251));
#92101=CARTESIAN_POINT('Ctrl Pts',(4.83327086321585,-8.20230696034932,3.94877530512736));
#92102=CARTESIAN_POINT('Ctrl Pts',(4.62864018694421,-8.31949579925618,3.94483449345222));
#92103=CARTESIAN_POINT('Ctrl Pts',(4.41997478684035,-8.42891624906166,3.94089368177707));
#92104=CARTESIAN_POINT('Ctrl Pts',(4.34272795189276,-8.46942312476701,3.93943481399699));
#92105=CARTESIAN_POINT('Ctrl Pts',(4.26492842864018,-8.50886583895404,3.93797594621691));
#92106=CARTESIAN_POINT('Ctrl Pts',(4.1866063912307,-8.54722956137872,3.93651707843683));
#92107=CARTESIAN_POINT('Ctrl Pts',(3.97426764245315,-8.65123738711385,3.9325619443609));
#92108=CARTESIAN_POINT('Ctrl Pts',(3.7580202469193,-8.74734377138224,3.92860681028497));
#92109=CARTESIAN_POINT('Ctrl Pts',(3.53847147788908,-8.83527169079511,3.92465167620904));
#92110=CARTESIAN_POINT('Ctrl Pts',(3.31895909650136,-8.923185037183,3.92069719765036));
#92111=CARTESIAN_POINT('Ctrl Pts',(3.09614669616946,-9.00292251954423,3.91674271909167));
#92112=CARTESIAN_POINT('Ctrl Pts',(2.87066135613154,-9.07425532087416,3.91278824053299));
#92113=CARTESIAN_POINT('Ctrl Pts',(2.6451990166122,-9.14558084593762,3.9088341653489));
#92114=CARTESIAN_POINT('Ctrl Pts',(2.41706455120558,-9.20850331658646,3.90488009016482));
#92115=CARTESIAN_POINT('Ctrl Pts',(2.18690098528352,-9.26284353374092,3.90092601498073));
#92116=CARTESIAN_POINT('Ctrl Pts',(1.95672016055529,-9.31718782559449,3.89697164330046));
#92117=CARTESIAN_POINT('Ctrl Pts',(1.72451020578604,-9.36294851051478,3.8930172716202));
#92118=CARTESIAN_POINT('Ctrl Pts',(1.49092635594465,-9.39999706655006,3.88906289993994));
#92119=CARTESIAN_POINT('Ctrl Pts',(1.2573443349623,-9.4370453325114,3.88510855922067));
#92120=CARTESIAN_POINT('Ctrl Pts',(1.02238871995914,-9.46538156400081,3.8811542185014));
#92121=CARTESIAN_POINT('Ctrl Pts',(0.786722634961963,-9.48492876861174,
3.87719987778213));
#92122=CARTESIAN_POINT('Ctrl Pts',(0.55101021466734,-9.50447981648055,3.87324475958334));
#92123=CARTESIAN_POINT('Ctrl Pts',(0.314587327016663,-9.51523836115445,
3.86928964138456));
#92124=CARTESIAN_POINT('Ctrl Pts',(0.0781211806985837,-9.5171793789508,
3.86533452318578));
#92125=CARTESIAN_POINT('Ctrl Pts',(-0.0415343703337308,-9.51816156417098,
3.86333317180909));
#92126=CARTESIAN_POINT('Ctrl Pts',(-0.161200965586209,-9.51688683390705,
3.8613318204324));
#92127=CARTESIAN_POINT('Ctrl Pts',(-0.280792149199087,-9.51335703203386,
3.85933046905572));
#92128=CARTESIAN_POINT('Ctrl Pts',(-0.517128894444723,-9.50638141844039,
3.85537538761769));
#92129=CARTESIAN_POINT('Ctrl Pts',(-0.753240109108659,-9.49059360653506,
3.85142030617966));
#92130=CARTESIAN_POINT('Ctrl Pts',(-0.988459419836826,-9.4660315985811,
3.84746522474164));
#92131=CARTESIAN_POINT('Ctrl Pts',(-1.22363961627426,-9.44147367500915,
3.84351080098858));
#92132=CARTESIAN_POINT('Ctrl Pts',(-1.45792792382192,-9.4081444973385,3.83955637723552));
#92133=CARTESIAN_POINT('Ctrl Pts',(-1.69066291833379,-9.36613394878437,
3.83560195348247));
#92134=CARTESIAN_POINT('Ctrl Pts',(-1.92337405506483,-9.32412770675262,
3.83164793509937));
#92135=CARTESIAN_POINT('Ctrl Pts',(-2.15453191862022,-9.27344192099779,
3.82769391671627));
#92136=CARTESIAN_POINT('Ctrl Pts',(-2.38348410703422,-9.21421780519189,
3.82373989833317));
#92137=CARTESIAN_POINT('Ctrl Pts',(-2.61245331344558,-9.15498928726233,
3.81978558604821));
#92138=CARTESIAN_POINT('Ctrl Pts',(-2.83921624277278,-9.08722123935626,
3.81583127376325));
#92139=CARTESIAN_POINT('Ctrl Pts',(-3.06313331524021,-9.01110540073001,
3.81187696147829));
#92140=CARTESIAN_POINT('Ctrl Pts',(-3.28704855605815,-8.93499018473399,
3.80792268153975));
#92141=CARTESIAN_POINT('Ctrl Pts',(-3.50811771966648,-8.85052740772846,
3.8039684016012));
#92142=CARTESIAN_POINT('Ctrl Pts',(-3.72571826786526,-8.75795807471668,
3.80001412166265));
#92143=CARTESIAN_POINT('Ctrl Pts',(-3.94336150501496,-8.66537058142108,
3.7960590659721));
#92144=CARTESIAN_POINT('Ctrl Pts',(-4.1575345068657,-8.56467346500325,3.79210401028154));
#92145=CARTESIAN_POINT('Ctrl Pts',(-4.36763534766171,-8.45615561114245,
3.78814895459099));
#92146=CARTESIAN_POINT('Ctrl Pts',(-4.47396975352136,-8.40123350101794,
3.78614725628553));
#92147=CARTESIAN_POINT('Ctrl Pts',(-4.57926143832089,-8.34430886723251,
3.78414555798007));
#92148=CARTESIAN_POINT('Ctrl Pts',(-4.68343473375798,-8.28542366717776,
3.78214385967461));
#92149=CARTESIAN_POINT('Ctrl Pts',(-4.88928158859004,-8.16906627273643,
3.77818849569411));
#92150=CARTESIAN_POINT('Ctrl Pts',(-5.09081992575374,-8.04501697995684,
3.77423313171361));
#92151=CARTESIAN_POINT('Ctrl Pts',(-5.2874778747596,-7.91362015603022,3.77027776773312));
#92152=CARTESIAN_POINT('Ctrl Pts',(-5.48410332337008,-7.78224504721225,
3.7663230574302));
#92153=CARTESIAN_POINT('Ctrl Pts',(-5.67584975902805,-7.64352498817002,
3.76236834712729));
#92154=CARTESIAN_POINT('Ctrl Pts',(-5.86217387975088,-7.49784793481213,
3.75841363682438));
#92155=CARTESIAN_POINT('Ctrl Pts',(-6.04847904865881,-7.35218569888389,
3.75445932877179));
#92156=CARTESIAN_POINT('Ctrl Pts',(-6.22936278134758,-7.19956805559108,
3.7505050207192));
#92157=CARTESIAN_POINT('Ctrl Pts',(-6.40431369012583,-7.04042416395965,
3.74655071266661));
#92158=CARTESIAN_POINT('Ctrl Pts',(-6.57927771753765,-6.88126833897837,
3.7425961081016));
#92159=CARTESIAN_POINT('Ctrl Pts',(-6.74830782127441,-6.71558547602045,
3.73864150353658));
#92160=CARTESIAN_POINT('Ctrl Pts',(-6.91092751357785,-6.54384345412332,
3.73468689897157));
#92161=CARTESIAN_POINT('Ctrl Pts',(-7.07354591645346,-6.37210279398589,
3.73073232576301));
#92162=CARTESIAN_POINT('Ctrl Pts',(-7.22975381691432,-6.19430327777564,
3.72677775255445));
#92163=CARTESIAN_POINT('Ctrl Pts',(-7.37911277218885,-6.01094842311256,
3.72282317934589));
#92164=CARTESIAN_POINT('Ctrl Pts',(-7.52850101353397,-5.82755761651606,
3.7188678307308));
#92165=CARTESIAN_POINT('Ctrl Pts',(-7.67103744775897,-5.63860951403788,
3.7149124821157));
#92166=CARTESIAN_POINT('Ctrl Pts',(-7.80632418994686,-5.44464038219702,
3.71095713350061));
#92167=CARTESIAN_POINT('Ctrl Pts',(-7.87472984615139,-5.34656288005296,
3.70895717243157));
#92168=CARTESIAN_POINT('Ctrl Pts',(-7.94128266403896,-5.24720216376444,
3.70695721136252));
#92169=CARTESIAN_POINT('Ctrl Pts',(-8.00593538759606,-5.14663043355915,
3.70495725029348));
#92170=CARTESIAN_POINT('Ctrl Pts',(-8.13379265773527,-4.9477397114093,3.70100212592124));
#92171=CARTESIAN_POINT('Ctrl Pts',(-8.25425339444311,-4.74405309913378,
3.697047001549));
#92172=CARTESIAN_POINT('Ctrl Pts',(-8.36697222093433,-4.53614176411114,
3.69309187717676));
#92173=CARTESIAN_POINT('Ctrl Pts',(-8.47967233150307,-4.32826495084983,
3.68913740951648));
#92174=CARTESIAN_POINT('Ctrl Pts',(-8.58463296330333,-4.11616506353748,
3.6851829418562));
#92175=CARTESIAN_POINT('Ctrl Pts',(-8.68155433255552,-3.90043851648587,
3.68122847419592));
#92176=CARTESIAN_POINT('Ctrl Pts',(-8.77846578695878,-3.68473403779898,
3.67727441106922));
#92177=CARTESIAN_POINT('Ctrl Pts',(-8.867339505136,-3.4654038979101,3.67332034794253));
#92178=CARTESIAN_POINT('Ctrl Pts',(-8.94792314470012,-3.24306608729145,
3.66936628481584));
#92179=CARTESIAN_POINT('Ctrl Pts',(-9.02851279306713,-3.02071169782274,
3.66541192685032));
#92180=CARTESIAN_POINT('Ctrl Pts',(-9.10081102881558,-2.79534945434882,
3.6614575688848));
#92181=CARTESIAN_POINT('Ctrl Pts',(-9.16461443518121,-2.56761533420958,
3.65750321091927));
#92182=CARTESIAN_POINT('Ctrl Pts',(-9.22841732703322,-2.33988305052884,
3.65354888484188));
#92183=CARTESIAN_POINT('Ctrl Pts',(-9.28372545245174,-2.10977920124336,
3.64959455876448));
#92184=CARTESIAN_POINT('Ctrl Pts',(-9.33038566644054,-1.87795355786051,
3.64564023268709));
#92185=CARTESIAN_POINT('Ctrl Pts',(-9.37705503894105,-1.64608241151724,
3.64168513045076));
#92186=CARTESIAN_POINT('Ctrl Pts',(-9.41507305247464,-1.41248907295379,
3.63773002821444));
#92187=CARTESIAN_POINT('Ctrl Pts',(-9.44433770997892,-1.17783337950249,
3.63377492597812));
#92188=CARTESIAN_POINT('Ctrl Pts',(-9.45914671157632,-1.05908889945336,
3.63177349762287));
#92189=CARTESIAN_POINT('Ctrl Pts',(-9.47171502900033,-0.940072506192662,
3.62977206926762));
#92190=CARTESIAN_POINT('Ctrl Pts',(-9.48203449694926,-0.820870299538334,
3.62777064091237));
#92191=CARTESIAN_POINT('Ctrl Pts',(-9.50373124089866,-0.570246937095671,
3.62356262565696));
#92192=CARTESIAN_POINT('Ctrl Pts',(-9.51548761186254,-0.318757908470078,
3.61935461040155));
#92193=CARTESIAN_POINT('Ctrl Pts',(-9.51726304323121,-0.0671596303259994,
3.61514659514614));
#92194=CARTESIAN_POINT('Ctrl Pts',(-9.5174205470755,-0.0448395920950911,
3.61477328948574));
#92195=CARTESIAN_POINT('Ctrl Pts',(-9.51749953482576,-0.0225186960109495,
3.61439998382535));
#92196=CARTESIAN_POINT('Ctrl Pts',(-9.51749999795141,-0.000197471173248046,
3.61402667816495));
#92197=CARTESIAN_POINT('Origin',(0.,0.,0.));
#92198=CARTESIAN_POINT('',(-9.51791998781483,-0.000166932759165794,2.61402667816495));
#92199=CARTESIAN_POINT('',(-9.51744795729939,-8.37115215137324E-5,2.88597332205635));
#92200=CARTESIAN_POINT('',(-9.5175,-1.16555759108849E-15,0.));
#92201=CARTESIAN_POINT('Ctrl Pts',(-9.51682764166119,-8.38638332260327E-5,
2.88597332469409));
#92202=CARTESIAN_POINT('Ctrl Pts',(-9.51704486858051,-0.666265069291475,
2.8971113726842));
#92203=CARTESIAN_POINT('Ctrl Pts',(-9.28852394762602,-2.87117666120216,
2.93397829046798));
#92204=CARTESIAN_POINT('Ctrl Pts',(-7.60322208917357,-6.33842508774048,
2.99657407804553));
#92205=CARTESIAN_POINT('Ctrl Pts',(-3.77155676659138,-9.15204736286997,
3.07376068742662));
#92206=CARTESIAN_POINT('Ctrl Pts',(0.929940046163851,-9.85493976609273,
3.15094729680775));
#92207=CARTESIAN_POINT('Ctrl Pts',(5.41696593703601,-8.28499142533159,3.22813390618885));
#92208=CARTESIAN_POINT('Ctrl Pts',(8.65467923647761,-4.80428494172239,3.30532051556997));
#92209=CARTESIAN_POINT('Ctrl Pts',(9.89637150055028,-0.21556083099493,3.38250712495109));
#92210=CARTESIAN_POINT('Ctrl Pts',(8.85566539917763,4.42286134570138,3.45969373433219));
#92211=CARTESIAN_POINT('Ctrl Pts',(5.77259141334861,8.04127457290448,3.53688034371332));
#92212=CARTESIAN_POINT('Ctrl Pts',(1.35817110792663,9.80506885261808,3.61406695309443));
#92213=CARTESIAN_POINT('Ctrl Pts',(-3.36944939868327,9.30765437281576,3.69125356247554));
#92214=CARTESIAN_POINT('Ctrl Pts',(-7.32004314469702,6.66336788144076,3.76844017185665));
#92215=CARTESIAN_POINT('Ctrl Pts',(-9.22237333027156,3.14792279530392,3.83334675830983));
#92216=CARTESIAN_POINT('Ctrl Pts',(-9.51671069117059,0.804315052831599,
3.87252447496929));
#92217=CARTESIAN_POINT('Ctrl Pts',(-9.51680985342271,-0.000133048433053571,
3.88597332183505));
#92218=CARTESIAN_POINT('Ctrl Pts',(-9.51773470173007,-0.000197284648878047,
3.61402667496411));
#92219=CARTESIAN_POINT('Ctrl Pts',(-9.51656296408864,1.26431828378534,3.59287912715316));
#92220=CARTESIAN_POINT('Ctrl Pts',(-8.95387422534848,4.06829986255365,3.54600270954852));
#92221=CARTESIAN_POINT('Ctrl Pts',(-6.27947569657596,7.65198082141816,3.47339742215013));
#92222=CARTESIAN_POINT('Ctrl Pts',(-1.98809297574734,9.69701483877292,3.39621081276903));
#92223=CARTESIAN_POINT('Ctrl Pts',(2.76180201423585,9.50563346318468,3.31902420338792));
#92224=CARTESIAN_POINT('Ctrl Pts',(6.87474452053818,7.12197324301039,3.2418375940068));
#92225=CARTESIAN_POINT('Ctrl Pts',(9.40216890275978,3.09577706353974,3.16465098462569));
#92226=CARTESIAN_POINT('Ctrl Pts',(9.76117699939271,-1.64439638338132,3.08746437524458));
#92227=CARTESIAN_POINT('Ctrl Pts',(7.86897092521903,-6.00532365023846,3.01027776586345));
#92228=CARTESIAN_POINT('Ctrl Pts',(4.16194902035729,-8.98124691528834,2.93309115648234));
#92229=CARTESIAN_POINT('Ctrl Pts',(-0.504940590312465,-9.88583080328021,
2.85590454710123));
#92230=CARTESIAN_POINT('Ctrl Pts',(-5.05537606528319,-8.51045172514667,
2.77871793772012));
#92231=CARTESIAN_POINT('Ctrl Pts',(-8.43989332168798,-5.17231248367099,
2.701531328339));
#92232=CARTESIAN_POINT('Ctrl Pts',(-9.46265691397307,-1.9497308459096,2.64663424182061));
#92233=CARTESIAN_POINT('Ctrl Pts',(-9.51809120030368,-0.205810744375301,
2.61746602509593));
#92234=CARTESIAN_POINT('Ctrl Pts',(-9.51791998781483,-0.000166932759165794,
2.61402667816495));
#92235=CARTESIAN_POINT('Origin',(0.,0.,0.));
#92236=CARTESIAN_POINT('',(-9.5175,4.49712710671297E-14,1.6143576464275));
#92237=CARTESIAN_POINT('',(-9.51749999907439,-0.000132736732560753,1.88597332185171));
#92238=CARTESIAN_POINT('',(-9.5175,-1.16555759108849E-15,0.));
#92239=CARTESIAN_POINT('Ctrl Pts',(-9.51749999907439,-0.000132736732560753,
1.88597332185171));
#92240=CARTESIAN_POINT('Ctrl Pts',(-9.51749661865394,-0.242515918735408,
1.8900256477718));
#92241=CARTESIAN_POINT('Ctrl Pts',(-9.50822970172581,-0.484864835621161,
1.89407797369188));
#92242=CARTESIAN_POINT('Ctrl Pts',(-9.48973308058393,-0.726479393562538,
1.89813029961196));
#92243=CARTESIAN_POINT('Ctrl Pts',(-9.47123110468,-0.968163898790906,1.90218379867825));
#92244=CARTESIAN_POINT('Ctrl Pts',(-9.44349410461844,-1.20911336980557,
1.90623729774455));
#92245=CARTESIAN_POINT('Ctrl Pts',(-9.40660785953286,-1.44863205368883,
1.91029079681084));
#92246=CARTESIAN_POINT('Ctrl Pts',(-9.38940686296382,-1.5603257229723,1.9121810467772));
#92247=CARTESIAN_POINT('Ctrl Pts',(-9.37021701025927,-1.67170834747593,
1.91407129674355));
#92248=CARTESIAN_POINT('Ctrl Pts',(-9.34905082871763,-1.78270997418374,
1.9159615467099));
#92249=CARTESIAN_POINT('Ctrl Pts',(-9.3047620390922,-2.01497329875517,1.91991676569613));
#92250=CARTESIAN_POINT('Ctrl Pts',(-9.25180717594818,-2.24561919650383,
1.92387198468235));
#92251=CARTESIAN_POINT('Ctrl Pts',(-9.19032924885024,-2.4739956644521,1.92782720366858));
#92252=CARTESIAN_POINT('Ctrl Pts',(-9.12886151153041,-2.70233427970032,
1.93178176708937));
#92253=CARTESIAN_POINT('Ctrl Pts',(-9.05887360372417,-2.92840394323743,
1.93573633051016));
#92254=CARTESIAN_POINT('Ctrl Pts',(-8.98055897850418,-3.1515657511161,1.93969089393095));
#92255=CARTESIAN_POINT('Ctrl Pts',(-8.90225234766956,-3.37470477855642,
1.94364505366848));
#92256=CARTESIAN_POINT('Ctrl Pts',(-8.81562079020307,-3.59493627644656,
1.947599213406));
#92257=CARTESIAN_POINT('Ctrl Pts',(-8.7209070145311,-3.81163837396759,1.95155337314352));
#92258=CARTESIAN_POINT('Ctrl Pts',(-8.62618616259571,-4.0283566617536,1.95550782830456));
#92259=CARTESIAN_POINT('Ctrl Pts',(-8.52338199664531,-4.24154476222042,
1.95946228346559));
#92260=CARTESIAN_POINT('Ctrl Pts',(-8.41278508446992,-4.45060146188361,
1.96341673862662));
#92261=CARTESIAN_POINT('Ctrl Pts',(-8.30218905947044,-4.65965648455541,
1.96737116206617));
#92262=CARTESIAN_POINT('Ctrl Pts',(-8.18380054746117,-4.86457992394017,
1.97132558550573));
#92263=CARTESIAN_POINT('Ctrl Pts',(-8.05795606390058,-5.06479519055291,
1.97528000894529));
#92264=CARTESIAN_POINT('Ctrl Pts',(-7.93208689157643,-5.26504973633976,
1.97923520818226));
#92265=CARTESIAN_POINT('Ctrl Pts',(-7.79875897531133,-5.46059402434427,
1.98319040741923));
#92266=CARTESIAN_POINT('Ctrl Pts',(-7.65835284563321,-5.65087939543765,
1.9871456066562));
#92267=CARTESIAN_POINT('Ctrl Pts',(-7.58732441917897,-5.74714065210079,
1.98914645646781));
#92268=CARTESIAN_POINT('Ctrl Pts',(-7.51448526741096,-5.8420565548024,1.99114730627942));
#92269=CARTESIAN_POINT('Ctrl Pts',(-7.43988872314389,-5.93555911749149,
1.99314815609103));
#92270=CARTESIAN_POINT('Ctrl Pts',(-7.29242854574708,-6.12039213645585,
1.99710337507688));
#92271=CARTESIAN_POINT('Ctrl Pts',(-7.13805564648719,-6.2997542161798,2.00105859406273));
#92272=CARTESIAN_POINT('Ctrl Pts',(-6.97720050024153,-6.4731352086473,2.00501381304859));
#92273=CARTESIAN_POINT('Ctrl Pts',(-6.8163720152435,-6.64648746374655,2.00896837646901));
#92274=CARTESIAN_POINT('Ctrl Pts',(-6.64906362018808,-6.81386040344975,
2.01292293988944));
#92275=CARTESIAN_POINT('Ctrl Pts',(-6.47574430996344,-6.97477898445364,
2.01687750330986));
#92276=CARTESIAN_POINT('Ctrl Pts',(-6.30244269223591,-7.13568113883128,
2.02083166304704));
#92277=CARTESIAN_POINT('Ctrl Pts',(-6.12313159158954,-7.29013005785499,
2.02478582278421));
#92278=CARTESIAN_POINT('Ctrl Pts',(-5.93831563774861,-7.43768872946901,
2.02873998252139));
#92279=CARTESIAN_POINT('Ctrl Pts',(-5.7534858759237,-7.58525842549803,2.03269443768206));
#92280=CARTESIAN_POINT('Ctrl Pts',(-5.56315065832492,-7.72593666706023,
2.03664889284273));
#92281=CARTESIAN_POINT('Ctrl Pts',(-5.36784732493689,-7.85932702883446,
2.04060334800339));
#92282=CARTESIAN_POINT('Ctrl Pts',(-5.17254555821376,-7.99271632059112,
2.04455777144261));
#92283=CARTESIAN_POINT('Ctrl Pts',(-4.97227599009689,-8.11881769196253,
2.04851219488182));
#92284=CARTESIAN_POINT('Ctrl Pts',(-4.76760513036824,-8.2372779224017,2.05246661832103));
#92285=CARTESIAN_POINT('Ctrl Pts',(-4.56289411734637,-8.3557613929268,2.05642181755766));
#92286=CARTESIAN_POINT('Ctrl Pts',(-4.35378033202857,-8.46660058548498,
2.06037701679428));
#92287=CARTESIAN_POINT('Ctrl Pts',(-4.14085620286599,-8.56948750843283,
2.06433221603091));
#92288=CARTESIAN_POINT('Ctrl Pts',(-4.03314248765502,-8.62153577915219,
2.06633306584466));
#92289=CARTESIAN_POINT('Ctrl Pts',(-3.92445403915644,-8.67154969530967,
2.0683339156584));
#92290=CARTESIAN_POINT('Ctrl Pts',(-3.81486973445662,-8.71949397379956,
2.07033476547215));
#92291=CARTESIAN_POINT('Ctrl Pts',(-3.59824681779616,-8.81426876360283,
2.07428998445757));
#92292=CARTESIAN_POINT('Ctrl Pts',(-3.37805880764698,-8.90098086104498,
2.07824520344299));
#92293=CARTESIAN_POINT('Ctrl Pts',(-3.15492436404717,-8.97937962818933,
2.08220042242841));
#92294=CARTESIAN_POINT('Ctrl Pts',(-2.93182690429828,-9.05776540097804,
2.08615498584839));
#92295=CARTESIAN_POINT('Ctrl Pts',(-2.70578425252372,-9.12784050045745,
2.09010954926838));
#92296=CARTESIAN_POINT('Ctrl Pts',(-2.47743278142928,-9.18940330290817,
2.09406411268836));
#92297=CARTESIAN_POINT('Ctrl Pts',(-2.2491046205356,-9.25095982100576,2.09801827242508));
#92298=CARTESIAN_POINT('Ctrl Pts',(-2.01846838372202,-9.30400570358082,
2.1019724321618));
#92299=CARTESIAN_POINT('Ctrl Pts',(-1.78617423957292,-9.34838958515776,
2.10592659189852));
#92300=CARTESIAN_POINT('Ctrl Pts',(-1.55386274024469,-9.3927767827469,2.10988104705874));
#92301=CARTESIAN_POINT('Ctrl Pts',(-1.31989336320424,-9.42850063055647,
2.11383550221897));
#92302=CARTESIAN_POINT('Ctrl Pts',(-1.08492629424608,-9.45546091875237,
2.11778995737919));
#92303=CARTESIAN_POINT('Ctrl Pts',(-0.849961110124046,-9.48242099068084,
2.12174438081795));
#92304=CARTESIAN_POINT('Ctrl Pts',(-0.613998531151393,-9.5006176136475,
2.12569880425671));
#92305=CARTESIAN_POINT('Ctrl Pts',(-0.377704407636725,-9.51000239907708,
2.12965322769547));
#92306=CARTESIAN_POINT('Ctrl Pts',(-0.141363926827158,-9.5193890256581,
2.13360842693166));
#92307=CARTESIAN_POINT('Ctrl Pts',(0.095307946013853,-9.51996034913527,
2.13756362616785));
#92308=CARTESIAN_POINT('Ctrl Pts',(0.331643515915196,-9.51172007727054,
2.14151882540404));
#92309=CARTESIAN_POINT('Ctrl Pts',(0.451200573198273,-9.50755150181755,
2.14351967522044));
#92310=CARTESIAN_POINT('Ctrl Pts',(0.570671569610272,-9.50112875311945,
2.14552052503685));
#92311=CARTESIAN_POINT('Ctrl Pts',(0.689970275166106,-9.49245738833666,
2.14752137485325));
#92312=CARTESIAN_POINT('Ctrl Pts',(0.925796323506403,-9.47531609848851,
2.15147659384181));
#92313=CARTESIAN_POINT('Ctrl Pts',(1.16101762167841,-9.44937985683982,2.15543181283037));
#92314=CARTESIAN_POINT('Ctrl Pts',(1.39497000565972,-9.41471534000417,2.15938703181893));
#92315=CARTESIAN_POINT('Ctrl Pts',(1.6288836127502,-9.38005656870596,2.16334159524207));
#92316=CARTESIAN_POINT('Ctrl Pts',(1.86152844603758,-9.33667245155772,2.1672961586652));
#92317=CARTESIAN_POINT('Ctrl Pts',(2.09224752123643,-9.28468128477656,2.17125072208833));
#92318=CARTESIAN_POINT('Ctrl Pts',(2.32294304454896,-9.23269542527243,2.1752048818282));
#92319=CARTESIAN_POINT('Ctrl Pts',(2.5517129266733,-9.17210433261013,2.17915904156808));
#92320=CARTESIAN_POINT('Ctrl Pts',(2.77791140813789,-9.10307719721949,2.18311320130795));
#92321=CARTESIAN_POINT('Ctrl Pts',(3.0041267893614,-9.03404490466802,2.18706765647132));
#92322=CARTESIAN_POINT('Ctrl Pts',(3.22777011493119,-8.95657538995117,2.19102211163469));
#92323=CARTESIAN_POINT('Ctrl Pts',(3.44821061147869,-8.87088777005356,2.19497656679806));
#92324=CARTESIAN_POINT('Ctrl Pts',(3.66864933971731,-8.78520083751685,2.19893099023995));
#92325=CARTESIAN_POINT('Ctrl Pts',(3.8858850277074,-8.69129603618083,2.20288541368184));
#92326=CARTESIAN_POINT('Ctrl Pts',(4.09930604925287,-8.58944096926912,2.20683983712373));
#92327=CARTESIAN_POINT('Ctrl Pts',(4.31276894073802,-8.48756591995138,2.21079503636301));
#92328=CARTESIAN_POINT('Ctrl Pts',(4.52241541524672,-8.37773761022079,2.21475023560229));
#92329=CARTESIAN_POINT('Ctrl Pts',(4.72765650136042,-8.26027059212618,2.21870543484157));
#92330=CARTESIAN_POINT('Ctrl Pts',(4.83148353023195,-8.2008465668976,2.22070628463917));
#92331=CARTESIAN_POINT('Ctrl Pts',(4.93418355225682,-8.13946842834864,2.22270713443677));
#92332=CARTESIAN_POINT('Ctrl Pts',(5.03568287172116,-8.07618129226023,2.22470798423436));
#92333=CARTESIAN_POINT('Ctrl Pts',(5.23632363706051,-7.95107720793802,2.22866320321354));
#92334=CARTESIAN_POINT('Ctrl Pts',(5.43232928174857,-7.81847428665558,2.23261842219272));
#92335=CARTESIAN_POINT('Ctrl Pts',(5.62314331351494,-7.67874114198885,2.2365736411719));
#92336=CARTESIAN_POINT('Ctrl Pts',(5.81392571843859,-7.53903115766389,2.24052820458562));
#92337=CARTESIAN_POINT('Ctrl Pts',(5.99951800026322,-7.39219347604901,2.24448276799933));
#92338=CARTESIAN_POINT('Ctrl Pts',(6.17939408300175,-7.23863903071309,2.24843733141305));
#92339=CARTESIAN_POINT('Ctrl Pts',(6.35925180392463,-7.08510026027056,2.25239149114351));
#92340=CARTESIAN_POINT('Ctrl Pts',(6.53339427600142,-6.92484627861794,2.25634565087396));
#92341=CARTESIAN_POINT('Ctrl Pts',(6.70132907997949,-6.75832781180532,2.26029981060441));
#92342=CARTESIAN_POINT('Ctrl Pts',(6.86927643071827,-6.59179690404951,2.26425426575841));
#92343=CARTESIAN_POINT('Ctrl Pts',(7.03101498405441,-6.41900077305369,2.26820872091242));
#92344=CARTESIAN_POINT('Ctrl Pts',(7.18608885391577,-6.24042732780597,2.27216317606642));
#92345=CARTESIAN_POINT('Ctrl Pts',(7.34116147982196,-6.06185531501984,2.27611759949899));
#92346=CARTESIAN_POINT('Ctrl Pts',(7.48956934558283,-5.87750629557614,2.28007202293156));
#92347=CARTESIAN_POINT('Ctrl Pts',(7.63089610808493,-5.68790214733115,2.28402644636413));
#92348=CARTESIAN_POINT('Ctrl Pts',(7.77225059674074,-5.49826080164624,2.28798164559423));
#92349=CARTESIAN_POINT('Ctrl Pts',(7.90652103730829,-5.3033624937494,2.29193684482432));
#92350=CARTESIAN_POINT('Ctrl Pts',(8.03333301603455,-5.10376007503186,2.29589204405441));
#92351=CARTESIAN_POINT('Ctrl Pts',(8.09748445678891,-5.00278552304238,2.2978928939081));
#92352=CARTESIAN_POINT('Ctrl Pts',(8.1597278654975,-4.90060759347963,2.29989374376179));
#92353=CARTESIAN_POINT('Ctrl Pts',(8.2200190771079,-4.79730055572737,2.30189459361549));
#92354=CARTESIAN_POINT('Ctrl Pts',(8.33920090638921,-4.59308635256111,2.30584981261525));
#92355=CARTESIAN_POINT('Ctrl Pts',(8.45078623942393,-4.38439887927302,2.30980503161502));
#92356=CARTESIAN_POINT('Ctrl Pts',(8.55445459915314,-4.17182367329058,2.31376025061478));
#92357=CARTESIAN_POINT('Ctrl Pts',(8.65810577617019,-3.95928370099551,2.31771481404915));
#92358=CARTESIAN_POINT('Ctrl Pts',(8.75384247554235,-3.74285753626607,2.32166937748351));
#92359=CARTESIAN_POINT('Ctrl Pts',(8.84139085815206,-3.52315397667845,2.32562394091788));
#92360=CARTESIAN_POINT('Ctrl Pts',(8.92893030379139,-3.30347284450921,2.32957810066899));
#92361=CARTESIAN_POINT('Ctrl Pts',(9.00828299709468,-3.08051524797425,2.3335322604201));
#92362=CARTESIAN_POINT('Ctrl Pts',(9.07922342536782,-2.85490949808435,2.33748642017121));
#92363=CARTESIAN_POINT('Ctrl Pts',(9.15016915374615,-2.62928689272523,2.34144087534572));
#92364=CARTESIAN_POINT('Ctrl Pts',(9.21270127393181,-2.40101600751153,2.34539533052023));
#92365=CARTESIAN_POINT('Ctrl Pts',(9.2666439278642,-2.17074101729745,2.34934978569474));
#92366=CARTESIAN_POINT('Ctrl Pts',(9.32058614908351,-1.94046787428577,2.3533042091477));
#92367=CARTESIAN_POINT('Ctrl Pts',(9.36593897961776,-1.70819093414095,2.35725863260066));
#92368=CARTESIAN_POINT('Ctrl Pts',(9.40257738038337,-1.47456598899577,2.36121305605362));
#92369=CARTESIAN_POINT('Ctrl Pts',(9.43922296904109,-1.24089521022067,2.3651682553038));
#92370=CARTESIAN_POINT('Ctrl Pts',(9.46715066796878,-1.00587617730016,2.36912345455397));
#92371=CARTESIAN_POINT('Ctrl Pts',(9.48628697188397,-0.770172537204796,
2.37307865380415));
#92372=CARTESIAN_POINT('Ctrl Pts',(9.49596761402503,-0.650935165075816,
2.37507950353496));
#92373=CARTESIAN_POINT('Ctrl Pts',(9.50339924749681,-0.531522685471028,
2.37708035326578));
#92374=CARTESIAN_POINT('Ctrl Pts',(9.50857742367356,-0.41202139265514,2.3790812029966));
#92375=CARTESIAN_POINT('Ctrl Pts',(9.51881348503294,-0.175794867323725,
2.38303642196104));
#92376=CARTESIAN_POINT('Ctrl Pts',(9.5202436499388,0.0608476937335277,2.38699164092549));
#92377=CARTESIAN_POINT('Ctrl Pts',(9.51285736796984,0.297238871384691,2.39094685988993));
#92378=CARTESIAN_POINT('Ctrl Pts',(9.50547231025459,0.53359086791902,2.3949014232889));
#92379=CARTESIAN_POINT('Ctrl Pts',(9.48927373159097,0.769691281850639,2.39885598668786));
#92380=CARTESIAN_POINT('Ctrl Pts',(9.46430318507777,1.00487385821641,2.40281055008682));
#92381=CARTESIAN_POINT('Ctrl Pts',(9.43933518756685,1.2400324270611,2.40676470980255));
#92382=CARTESIAN_POINT('Ctrl Pts',(9.40559704001639,1.47427306446482,2.41071886951827));
#92383=CARTESIAN_POINT('Ctrl Pts',(9.3631821461448,1.70693478144754,2.414673029234));
#92384=CARTESIAN_POINT('Ctrl Pts',(9.32076408336619,1.93961388108241,2.41862748437341));
#92385=CARTESIAN_POINT('Ctrl Pts',(9.26966802701636,2.17071354604124,2.42258193951283));
#92386=CARTESIAN_POINT('Ctrl Pts',(9.21003870508313,2.39958190126337,2.42653639465224));
#92387=CARTESIAN_POINT('Ctrl Pts',(9.1504098614765,2.62844842057961,2.43049081807033));
#92388=CARTESIAN_POINT('Ctrl Pts',(9.08224796266383,2.8550833930223,2.43444524148842));
#92389=CARTESIAN_POINT('Ctrl Pts',(9.00574811127941,3.07884835712761,2.43839966490651));
#92390=CARTESIAN_POINT('Ctrl Pts',(8.92923325178689,3.30265722051782,2.44235486412237));
#92391=CARTESIAN_POINT('Ctrl Pts',(8.84437726259469,3.52359468298996,2.44631006333823));
#92392=CARTESIAN_POINT('Ctrl Pts',(8.75142449937058,3.74103935849604,2.45026526255409));
#92393=CARTESIAN_POINT('Ctrl Pts',(8.70440170211514,3.851039927989,2.4522661124953));
#92394=CARTESIAN_POINT('Ctrl Pts',(8.65530760636025,3.96014694989684,2.45426696243651));
#92395=CARTESIAN_POINT('Ctrl Pts',(8.6041785058948,4.06828200702679,2.45626781237772));
#92396=CARTESIAN_POINT('Ctrl Pts',(8.50310806286357,4.2820400827965,2.46022303138521));
#92397=CARTESIAN_POINT('Ctrl Pts',(8.39405322125943,4.4920610098125,2.4641782503927));
#92398=CARTESIAN_POINT('Ctrl Pts',(8.27731579054074,4.69774941367299,2.4681334694002));
#92399=CARTESIAN_POINT('Ctrl Pts',(8.16059770869367,4.9034037253105,2.47208803284226));
#92400=CARTESIAN_POINT('Ctrl Pts',(8.03619971911926,5.10472670159992,2.47604259628431));
#92401=CARTESIAN_POINT('Ctrl Pts',(7.90446918377241,5.30114828813459,2.47999715972637));
#92402=CARTESIAN_POINT('Ctrl Pts',(7.77275209552822,5.49754982387976,2.4839513194851));
#92403=CARTESIAN_POINT('Ctrl Pts',(7.63370411346527,5.68905073426294,2.48790547924383));
#92404=CARTESIAN_POINT('Ctrl Pts',(7.4877160160783,5.87510979578804,2.49185963900257));
#92405=CARTESIAN_POINT('Ctrl Pts',(7.34171701162601,6.06118275816104,2.49581409418455));
#92406=CARTESIAN_POINT('Ctrl Pts',(7.18877702816723,6.24181283526938,2.49976854936654));
#92407=CARTESIAN_POINT('Ctrl Pts',(7.02932800121784,6.41649079336165,2.50372300454853));
#92408=CARTESIAN_POINT('Ctrl Pts',(6.86988025332853,6.59116735023118,2.50767742800887));
#92409=CARTESIAN_POINT('Ctrl Pts',(6.70392375861793,6.75989167636968,2.5116318514692));
#92410=CARTESIAN_POINT('Ctrl Pts',(6.53192876504471,6.92218988892832,2.51558627492954));
#92411=CARTESIAN_POINT('Ctrl Pts',(6.35990002870103,7.08451994189825,2.5195414741869));
#92412=CARTESIAN_POINT('Ctrl Pts',(6.18183063194394,7.24042116815391,2.52349667344426));
#92413=CARTESIAN_POINT('Ctrl Pts',(5.99822643580178,7.38945775242329,2.52745187270162));
#92414=CARTESIAN_POINT('Ctrl Pts',(5.90534504747037,7.46485213419654,2.52945272238735));
#92415=CARTESIAN_POINT('Ctrl Pts',(5.81104777392244,7.53849039205081,2.53145357207309));
#92416=CARTESIAN_POINT('Ctrl Pts',(5.71540328092111,7.61032007122146,2.53345442175882));
#92417=CARTESIAN_POINT('Ctrl Pts',(5.52633614700454,7.75231080319966,2.53740964075376));
#92418=CARTESIAN_POINT('Ctrl Pts',(5.33194754946568,7.88727309826655,2.54136485974869));
#92419=CARTESIAN_POINT('Ctrl Pts',(5.13278205151137,8.01482093759323,2.54532007874363));
#92420=CARTESIAN_POINT('Ctrl Pts',(4.93364956461967,8.14234763626174,2.5492746421733));
#92421=CARTESIAN_POINT('Ctrl Pts',(4.72974199575358,8.26246218005756,2.55322920560298));
#92422=CARTESIAN_POINT('Ctrl Pts',(4.52163240384909,8.37482218643846,2.55718376903265));
#92423=CARTESIAN_POINT('Ctrl Pts',(4.31354405583911,8.48717072307354,2.56113792877921));
#92424=CARTESIAN_POINT('Ctrl Pts',(4.10125478989817,8.59176616866206,2.56509208852577));
#92425=CARTESIAN_POINT('Ctrl Pts',(3.88536263429271,8.68831188724496,2.56904624827233));
#92426=CARTESIAN_POINT('Ctrl Pts',(3.66945434892627,8.78486481896332,2.57300070344255));
#92427=CARTESIAN_POINT('Ctrl Pts',(3.44994289296842,8.87336670414171,2.57695515861277));
#92428=CARTESIAN_POINT('Ctrl Pts',(3.22744779244037,8.9535683946163,2.580909613783));
#92429=CARTESIAN_POINT('Ctrl Pts',(3.00495447669792,9.03376944173819,2.58486403723183));
#92430=CARTESIAN_POINT('Ctrl Pts',(2.77947783092414,9.1056703336265,2.58881846068065));
#92431=CARTESIAN_POINT('Ctrl Pts',(2.55165479540441,9.16907105736943,2.59277288412948));
#92432=CARTESIAN_POINT('Ctrl Pts',(2.32378706448556,9.23248421936578,2.59672808337578));
#92433=CARTESIAN_POINT('Ctrl Pts',(2.09357229636057,9.28739380525412,2.60068328262208));
#92434=CARTESIAN_POINT('Ctrl Pts',(1.86166119100045,9.33365008235914,2.60463848186838));
#92435=CARTESIAN_POINT('Ctrl Pts',(1.74434237848203,9.35705013253379,2.60663933162557));
#92436=CARTESIAN_POINT('Ctrl Pts',(1.6265896381928,9.37823649583386,2.60864018138276));
#92437=CARTESIAN_POINT('Ctrl Pts',(1.50848817155244,9.3971947775007,2.61064103113995));
#92438=CARTESIAN_POINT('Ctrl Pts',(1.27502878868999,9.43467093138751,2.61459625001065));
#92439=CARTESIAN_POINT('Ctrl Pts',(1.0401381629618,9.4634483247574,2.61855146888136));
#92440=CARTESIAN_POINT('Ctrl Pts',(0.804478019009862,9.4834393216243,2.62250668775207));
#92441=CARTESIAN_POINT('Ctrl Pts',(0.568856935043161,9.50342700504146,2.62646125105672));
#92442=CARTESIAN_POINT('Ctrl Pts',(0.332466868962747,9.51463117523941,2.63041581436137));
#92443=CARTESIAN_POINT('Ctrl Pts',(0.0959744124212834,9.51701608500061,
2.63437037766602));
#92444=CARTESIAN_POINT('Ctrl Pts',(-0.140493902868283,9.5194007513092,2.63832453728715));
#92445=CARTESIAN_POINT('Ctrl Pts',(-0.377064305227066,9.51296795195225,
2.64227869690828));
#92446=CARTESIAN_POINT('Ctrl Pts',(-0.613069439541559,9.49773405146197,
2.6462328565294));
#92447=CARTESIAN_POINT('Ctrl Pts',(-0.849092206317806,9.48249901281354,
2.65018731157447));
#92448=CARTESIAN_POINT('Ctrl Pts',(-1.08454933842956,9.45846157469296,2.65414176661955));
#92449=CARTESIAN_POINT('Ctrl Pts',(-1.31877660028806,9.42569013539766,2.65809622166462));
#92450=CARTESIAN_POINT('Ctrl Pts',(-1.55300198327195,9.39291895898134,2.66205064498868));
#92451=CARTESIAN_POINT('Ctrl Pts',(-1.78599723613496,9.3514139629418,2.66600506831275));
#92452=CARTESIAN_POINT('Ctrl Pts',(-2.01710562344348,9.30129513314531,2.66995949163681));
#92453=CARTESIAN_POINT('Ctrl Pts',(-2.24825935076771,9.25116647078258,2.6739146907597));
#92454=CARTESIAN_POINT('Ctrl Pts',(-2.47752519658103,9.19242065784401,2.67786988988259));
#92455=CARTESIAN_POINT('Ctrl Pts',(-2.70425769253583,9.12522857699251,2.68182508900548));
#92456=CARTESIAN_POINT('Ctrl Pts',(-2.81895680501513,9.09123754272612,2.68382593951067));
#92457=CARTESIAN_POINT('Ctrl Pts',(-2.93300781075947,9.05508579835512,2.68582679001586));
#92458=CARTESIAN_POINT('Ctrl Pts',(-3.04632862255624,9.01680032901886,2.68782764052105));
#92459=CARTESIAN_POINT('Ctrl Pts',(-3.27033769614246,8.94111879813458,2.69178285987525));
#92460=CARTESIAN_POINT('Ctrl Pts',(-3.49155770459215,8.85707437037551,2.69573807922945));
#92461=CARTESIAN_POINT('Ctrl Pts',(-3.70936237479386,8.7648980041107,2.69969329858366));
#92462=CARTESIAN_POINT('Ctrl Pts',(-3.9271309446225,8.67273691576076,2.70364786237389));
#92463=CARTESIAN_POINT('Ctrl Pts',(-4.14148504606553,8.57244668962403,2.70760242616412));
#92464=CARTESIAN_POINT('Ctrl Pts',(-4.35181829019908,8.46430645824505,2.71155698995435));
#92465=CARTESIAN_POINT('Ctrl Pts',(-4.56213006345908,8.35617726584966,2.71551115006166));
#92466=CARTESIAN_POINT('Ctrl Pts',(-4.76842154770438,8.24019979745532,2.71946531016896));
#92467=CARTESIAN_POINT('Ctrl Pts',(-4.97010997249879,8.11669964402208,2.72341947027627));
#92468=CARTESIAN_POINT('Ctrl Pts',(-5.17181346574513,7.99319026370272,2.72737392580495));
#92469=CARTESIAN_POINT('Ctrl Pts',(-5.36891296993222,7.86215722064698,2.73132838133363));
#92470=CARTESIAN_POINT('Ctrl Pts',(-5.56085273197587,7.72397068503478,2.73528283686231));
#92471=CARTESIAN_POINT('Ctrl Pts',(-5.75279095424601,7.58578525797852,2.73923726066768));
#92472=CARTESIAN_POINT('Ctrl Pts',(-5.93956928911505,7.44044662013735,2.74319168447304));
#92473=CARTESIAN_POINT('Ctrl Pts',(-6.12066266831653,7.28836708396856,2.74714610827841));
#92474=CARTESIAN_POINT('Ctrl Pts',(-6.30179157503234,7.13625771231974,2.75110130787607));
#92475=CARTESIAN_POINT('Ctrl Pts',(-6.47723308103396,6.97740498165161,2.75505650747373));
#92476=CARTESIAN_POINT('Ctrl Pts',(-6.64649581339093,6.81226097948228,2.75901170707139));
#92477=CARTESIAN_POINT('Ctrl Pts',(-6.7321220694572,6.72871829751884,2.76101255468165));
#92478=CARTESIAN_POINT('Ctrl Pts',(-6.81616766093029,6.64356621178076,2.76301340229191));
#92479=CARTESIAN_POINT('Ctrl Pts',(-6.8985725468889,6.55686686347305,2.76501424990217));
#92480=CARTESIAN_POINT('Ctrl Pts',(-7.06146816113144,6.38548207927338,2.76896946805079));
#92481=CARTESIAN_POINT('Ctrl Pts',(-7.21799764663385,6.20799899698917,2.77292468619942));
#92482=CARTESIAN_POINT('Ctrl Pts',(-7.3677146191458,6.02491390318777,2.77687990434805));
#92483=CARTESIAN_POINT('Ctrl Pts',(-7.51740677642026,5.84185915531179,2.78083446692853));
#92484=CARTESIAN_POINT('Ctrl Pts',(-7.66028849593555,5.65320446816517,2.78478902950901));
#92485=CARTESIAN_POINT('Ctrl Pts',(-7.79595344294093,5.45947947752324,2.7887435920895));
#92486=CARTESIAN_POINT('Ctrl Pts',(-7.93160454121154,5.26577426240972,2.79269775098657));
#92487=CARTESIAN_POINT('Ctrl Pts',(-8.06004017588902,5.06700000870574,2.79665190988365));
#92488=CARTESIAN_POINT('Ctrl Pts',(-8.18089656553735,4.86371644259606,2.80060606878072));
#92489=CARTESIAN_POINT('Ctrl Pts',(-8.3017619847953,4.66041768844997,2.80456052310703));
#92490=CARTESIAN_POINT('Ctrl Pts',(-8.41504688079174,4.452609190299,2.80851497743335));
#92491=CARTESIAN_POINT('Ctrl Pts',(-8.52043215627187,4.24087751772772,2.81246943175966));
#92492=CARTESIAN_POINT('Ctrl Pts',(-8.62581658650851,4.02914754335209,2.81642385436924));
#92493=CARTESIAN_POINT('Ctrl Pts',(-8.72330139905377,3.81349471154006,2.82037827697882));
#92494=CARTESIAN_POINT('Ctrl Pts',(-8.81261428931502,3.59452856961254,2.8243326995884));
#92495=CARTESIAN_POINT('Ctrl Pts',(-8.90194470168324,3.37551946918093,2.82828789800778));
#92496=CARTESIAN_POINT('Ctrl Pts',(-8.98309988145253,3.15319602152038,2.83224309642717));
#92497=CARTESIAN_POINT('Ctrl Pts',(-9.05585587648387,2.92818725397687,2.83619829484655));
#92498=CARTESIAN_POINT('Ctrl Pts',(-9.09266166151467,2.81435987350209,2.83819914965879));
#92499=CARTESIAN_POINT('Ctrl Pts',(-9.12731875453222,2.69984556005899,2.84020000447104));
#92500=CARTESIAN_POINT('Ctrl Pts',(-9.1598030074911,2.58472728038319,2.84220085928328));
#92501=CARTESIAN_POINT('Ctrl Pts',(-9.22440370066167,2.35579418245803,2.84617991362596));
#92502=CARTESIAN_POINT('Ctrl Pts',(-9.28042584834167,2.12440861146206,2.85015896796863));
#92503=CARTESIAN_POINT('Ctrl Pts',(-9.32770455370037,1.89122553093949,2.85413802231131));
#92504=CARTESIAN_POINT('Ctrl Pts',(-9.37497426678215,1.65808680118366,2.85811631984903));
#92505=CARTESIAN_POINT('Ctrl Pts',(-9.4135038034141,1.42315151436673,2.86209461738675));
#92506=CARTESIAN_POINT('Ctrl Pts',(-9.4431792573843,1.18708540674502,2.86607291492447));
#92507=CARTESIAN_POINT('Ctrl Pts',(-9.4728517539696,0.95104282490803,2.87005081599455));
#92508=CARTESIAN_POINT('Ctrl Pts',(-9.49367189415953,0.713869920319275,
2.87402871706464));
#92509=CARTESIAN_POINT('Ctrl Pts',(-9.50557743464729,0.476239313711379,
2.87800661813472));
#92510=CARTESIAN_POINT('Ctrl Pts',(-9.51352533747236,0.317601831312081,
2.88066218603483));
#92511=CARTESIAN_POINT('Ctrl Pts',(-9.51750139653877,0.158760508638162,
2.88331775393494));
#92512=CARTESIAN_POINT('Ctrl Pts',(-9.51749999963197,-8.36987430888474E-5,
2.88597332183505));
#92513=CARTESIAN_POINT('Ctrl Pts',(-9.51749999860915,-0.000162710879915706,
2.61426907583));
#92514=CARTESIAN_POINT('Ctrl Pts',(-9.51750793601857,0.464122739643576,
2.6062757959423));
#92515=CARTESIAN_POINT('Ctrl Pts',(-9.48354236659388,0.927792039220556,
2.59820482324316));
#92516=CARTESIAN_POINT('Ctrl Pts',(-9.39663191626681,1.51774366931572,2.58812418496722));
#92517=CARTESIAN_POINT('Ctrl Pts',(-9.37467393353151,1.64794599472725,2.58590862243221));
#92518=CARTESIAN_POINT('Ctrl Pts',(-9.27630610838416,2.16533738281314,2.57713658796837));
#92519=CARTESIAN_POINT('Ctrl Pts',(-9.17855681534807,2.54806539167245,2.57073690299094));
#92520=CARTESIAN_POINT('Ctrl Pts',(-8.96282147259733,3.2164104855471,2.55938495258945));
#92521=CARTESIAN_POINT('Ctrl Pts',(-8.85416999457468,3.50444530344994,2.55442589450221));
#92522=CARTESIAN_POINT('Ctrl Pts',(-8.66174893614724,3.94814841316177,2.54639430837918));
#92523=CARTESIAN_POINT('Ctrl Pts',(-8.58727452692463,4.10761310330301,2.54341345597166));
#92524=CARTESIAN_POINT('Ctrl Pts',(-8.35047470048624,4.58002364993561,2.53436724317746));
#92525=CARTESIAN_POINT('Ctrl Pts',(-8.17514366886643,4.88611002607679,2.52823269237713));
#92526=CARTESIAN_POINT('Ctrl Pts',(-7.81529420596976,5.44050887824939,2.51687964908705));
#92527=CARTESIAN_POINT('Ctrl Pts',(-7.63486811434855,5.69093587142652,2.51164737487751));
#92528=CARTESIAN_POINT('Ctrl Pts',(-7.19841536251561,6.23851776600686,2.49998452723066));
#92529=CARTESIAN_POINT('Ctrl Pts',(-6.9355483207026,6.52950676514747,2.493629926593));
#92530=CARTESIAN_POINT('Ctrl Pts',(-6.43405315804867,7.02009481943592,2.48228989373565));
#92531=CARTESIAN_POINT('Ctrl Pts',(-6.20216587270621,7.22578077337415,2.47729788544506));
#92532=CARTESIAN_POINT('Ctrl Pts',(-5.82379944253089,7.52974017304037,2.46923870460397));
#92533=CARTESIAN_POINT('Ctrl Pts',(-5.68392075607238,7.63588046970078,2.4662652152463));
#92534=CARTESIAN_POINT('Ctrl Pts',(-5.25440320159795,7.94345475118456,2.45722245839205));
#92535=CARTESIAN_POINT('Ctrl Pts',(-4.95642331173384,8.13271757623477,2.45108329603022));
#92536=CARTESIAN_POINT('Ctrl Pts',(-4.37919983454863,8.45581156141909,2.43972032158993));
#92537=CARTESIAN_POINT('Ctrl Pts',(-4.10259279258243,8.59342042334503,2.43448279099346));
#92538=CARTESIAN_POINT('Ctrl Pts',(-3.45764823998831,8.87602382574983,2.42275448484561));
#92539=CARTESIAN_POINT('Ctrl Pts',(-3.08597433999832,9.01198613702497,2.41634306592113));
#92540=CARTESIAN_POINT('Ctrl Pts',(-2.41248762401099,9.21178765133125,2.40498796256226));
#92541=CARTESIAN_POINT('Ctrl Pts',(-2.11399843359201,9.28483370433371,2.40003744111097));
#92542=CARTESIAN_POINT('Ctrl Pts',(-1.63965098128222,9.37685198671634,2.39201296595234));
#92543=CARTESIAN_POINT('Ctrl Pts',(-1.46590359117822,9.40557993230006,2.38903016770001));
#92544=CARTESIAN_POINT('Ctrl Pts',(-0.942314241685625,9.47729077363448,
2.37998303650244));
#92545=CARTESIAN_POINT('Ctrl Pts',(-0.59078066399349,9.50568122664751,2.37384969792749));
#92546=CARTESIAN_POINT('Ctrl Pts',(0.0698136978474623,9.52223919566713,
2.36249926076456));
#92547=CARTESIAN_POINT('Ctrl Pts',(0.378305648054733,9.51497766278343,2.35726836399894));
#92548=CARTESIAN_POINT('Ctrl Pts',(1.07565873047447,9.46459025914108,2.34562344848382));
#92549=CARTESIAN_POINT('Ctrl Pts',(1.46331197777882,9.41245079619403,2.33928447787069));
#92550=CARTESIAN_POINT('Ctrl Pts',(2.15127981040714,9.27637988604303,2.32794850121074));
#92551=CARTESIAN_POINT('Ctrl Pts',(2.45276557221386,9.20125902427386,2.32294501131215));
#92552=CARTESIAN_POINT('Ctrl Pts',(2.91797376977633,9.06085024926193,2.31487616134734));
#92553=CARTESIAN_POINT('Ctrl Pts',(3.08447512671743,9.00553108062806,2.31190518397676));
#92554=CARTESIAN_POINT('Ctrl Pts',(3.58097263053224,8.82518690538203,2.30286359892522));
#92555=CARTESIAN_POINT('Ctrl Pts',(3.90563995603974,8.68638395756977,2.29672285411906));
#92556=CARTESIAN_POINT('Ctrl Pts',(4.49866219156555,8.39286845153751,2.28535646575933));
#92557=CARTESIAN_POINT('Ctrl Pts',(4.76864204310226,8.24246669790521,2.28011712558757));
#92558=CARTESIAN_POINT('Ctrl Pts',(5.36746836191316,7.86958414295812,2.26836720291976));
#92559=CARTESIAN_POINT('Ctrl Pts',(5.69067463900333,7.63912919155653,2.26193709783562));
#92560=CARTESIAN_POINT('Ctrl Pts',(6.23632658057496,7.19616738790312,2.25057693152237));
#92561=CARTESIAN_POINT('Ctrl Pts',(6.46463531907069,6.9917867905503,2.24563997288196));
#92562=CARTESIAN_POINT('Ctrl Pts',(6.80818548770489,6.65300533300363,2.23762676249105));
#92563=CARTESIAN_POINT('Ctrl Pts',(6.93021629669238,6.525792699333,2.23464083968749));
#92564=CARTESIAN_POINT('Ctrl Pts',(7.28536913966018,6.1343554266646,2.2255922292939));
#92565=CARTESIAN_POINT('Ctrl Pts',(7.50742580846015,5.8605015631703,2.21946083160097));
#92566=CARTESIAN_POINT('Ctrl Pts',(7.89436179833537,5.32511875410795,2.20811456333893));
#92567=CARTESIAN_POINT('Ctrl Pts',(8.06269030460154,5.06664236285625,2.20288586837272));
#92568=CARTESIAN_POINT('Ctrl Pts',(8.41445230070014,4.46444022242666,2.19127043535467));
#92569=CARTESIAN_POINT('Ctrl Pts',(8.58993370844498,4.11670673748643,2.18495722699093));
#92570=CARTESIAN_POINT('Ctrl Pts',(8.86676559282271,3.47281665013247,2.17362784763163));
#92571=CARTESIAN_POINT('Ctrl Pts',(8.97575005238465,3.18054971855134,2.16860536408051));
#92572=CARTESIAN_POINT('Ctrl Pts',(9.12327202495145,2.71650624104769,2.16052045931768));
#92573=CARTESIAN_POINT('Ctrl Pts',(9.17172841210101,2.54811601545726,2.15755357796201));
#92574=CARTESIAN_POINT('Ctrl Pts',(9.3037177426002,2.03671977214956,2.14851389567492));
#92575=CARTESIAN_POINT('Ctrl Pts',(9.37284594708001,1.69031090114701,2.14237056044812));
#92576=CARTESIAN_POINT('Ctrl Pts',(9.46611043193154,1.03491904538352,2.13099857671449));
#92577=CARTESIAN_POINT('Ctrl Pts',(9.49472104373032,0.727033896911485,2.12575626767931));
#92578=CARTESIAN_POINT('Ctrl Pts',(9.52581608644059,0.0202217071744701,
2.11397171439774));
#92579=CARTESIAN_POINT('Ctrl Pts',(9.51831238536809,-0.378565470332814,
2.10751174711588));
#92580=CARTESIAN_POINT('Ctrl Pts',(9.46098874159688,-1.07955511888953,2.09614338615257));
#92581=CARTESIAN_POINT('Ctrl Pts',(9.42155678110355,-1.38203223701904,2.09122802465508));
#92582=CARTESIAN_POINT('Ctrl Pts',(9.33647784150751,-1.85584217956872,2.08323266696666));
#92583=CARTESIAN_POINT('Ctrl Pts',(9.30045110827429,-2.02868837834661,2.08024168338257));
#92584=CARTESIAN_POINT('Ctrl Pts',(9.17822857542973,-2.54301334937323,2.07119066573233));
#92585=CARTESIAN_POINT('Ctrl Pts',(9.07786909989473,-2.88081414296955,2.06506239715364));
#92586=CARTESIAN_POINT('Ctrl Pts',(8.85504339872357,-3.50227402478332,2.05372284037786));
#92587=CARTESIAN_POINT('Ctrl Pts',(8.73704430828451,-3.78705367301889,2.04849768585152));
#92588=CARTESIAN_POINT('Ctrl Pts',(8.44040208699418,-4.414939216129,2.03693218157599));
#92589=CARTESIAN_POINT('Ctrl Pts',(8.25424467058249,-4.75389546033557,2.03066279434049));
#92590=CARTESIAN_POINT('Ctrl Pts',(7.88047528540663,-5.34597074275425,2.01934437453605));
#92591=CARTESIAN_POINT('Ctrl Pts',(7.69992694305407,-5.60289361808539,2.01428937614376));
#92592=CARTESIAN_POINT('Ctrl Pts',(7.39956056908833,-5.98831105896093,2.00617681981901));
#92593=CARTESIAN_POINT('Ctrl Pts',(7.28832527603495,-6.12320825437251,2.00321678278712));
#92594=CARTESIAN_POINT('Ctrl Pts',(6.94130724951403,-6.52118219734963,1.99418025738971));
#92595=CARTESIAN_POINT('Ctrl Pts',(6.69453549425969,-6.77427183689836,1.98803256501737));
#92596=CARTESIAN_POINT('Ctrl Pts',(6.20635388392835,-7.22216363663306,1.97665115039945));
#92597=CARTESIAN_POINT('Ctrl Pts',(5.96838048269892,-7.42003452760417,1.97140382900469));
#92598=CARTESIAN_POINT('Ctrl Pts',(5.40029111145813,-7.84735032630688,1.95956278169603));
#92599=CARTESIAN_POINT('Ctrl Pts',(5.06443308118453,-8.06818258618791,1.95305428034658));
#92600=CARTESIAN_POINT('Ctrl Pts',(4.4527672262796,-8.41708086538624,1.94167234367945));
#92601=CARTESIAN_POINT('Ctrl Pts',(4.18290177044801,-8.55439753223893,1.93679189471401));
#92602=CARTESIAN_POINT('Ctrl Pts',(3.74556064042098,-8.7512804354366,1.92882516881779));
#92603=CARTESIAN_POINT('Ctrl Pts',(3.58217186807243,-8.81942045403042,1.92582577578345));
#92604=CARTESIAN_POINT('Ctrl Pts',(3.08860280501219,-9.00928000311882,1.91677072755454));
#92605=CARTESIAN_POINT('Ctrl Pts',(2.75347385538079,-9.11728995033518,1.91064761992418));
#92606=CARTESIAN_POINT('Ctrl Pts',(2.11543854411611,-9.28452681479049,1.89931910672918));
#92607=CARTESIAN_POINT('Ctrl Pts',(1.81413097599623,-9.34807194207792,1.89409976658499));
#92608=CARTESIAN_POINT('Ctrl Pts',(1.13389278176502,-9.45740004270625,1.88262577824753));
#92609=CARTESIAN_POINT('Ctrl Pts',(0.754217159231396,-9.49522439648685,
1.87643739650504));
#92610=CARTESIAN_POINT('Ctrl Pts',(0.0612225515307943,-9.52242609115569,
1.86522595191986));
#92611=CARTESIAN_POINT('Ctrl Pts',(-0.251264301273633,-9.51930728206631,
1.86019677271956));
#92612=CARTESIAN_POINT('Ctrl Pts',(-0.73302922742814,-9.49075739552366,
1.85219390454869));
#92613=CARTESIAN_POINT('Ctrl Pts',(-0.902726115623141,-9.47612221062986,
1.84931584692176));
#92614=CARTESIAN_POINT('Ctrl Pts',(-1.43621072314985,-9.41565212364951,
1.84013877049304));
#92615=CARTESIAN_POINT('Ctrl Pts',(-1.79779422730175,-9.35334929421928,
1.83375416030769));
#92616=CARTESIAN_POINT('Ctrl Pts',(-2.45498103473692,-9.20058696143206,
1.82216536762711));
#92617=CARTESIAN_POINT('Ctrl Pts',(-2.75151767060223,-9.11629774929942,
1.8169397630396));
#92618=CARTESIAN_POINT('Ctrl Pts',(-3.40985861879621,-8.89411167640492,
1.80536771529789));
#92619=CARTESIAN_POINT('Ctrl Pts',(-3.76839537704575,-8.74823159571515,
1.79909257082554));
#92620=CARTESIAN_POINT('Ctrl Pts',(-4.39975954854341,-8.44530858302767,
1.7877727304967));
#92621=CARTESIAN_POINT('Ctrl Pts',(-4.67558008643426,-8.29578627527581,
1.78272201927272));
#92622=CARTESIAN_POINT('Ctrl Pts',(-5.09293896594558,-8.04209897228491,
1.77461312084655));
#92623=CARTESIAN_POINT('Ctrl Pts',(-5.23982984286413,-7.9471734037367,1.77165219332543));
#92624=CARTESIAN_POINT('Ctrl Pts',(-5.67525620547695,-7.64846442593763,
1.76261525881214));
#92625=CARTESIAN_POINT('Ctrl Pts',(-5.95514508304704,-7.43261656040967,
1.75646813538162));
#92626=CARTESIAN_POINT('Ctrl Pts',(-6.45640735853107,-6.99951838564554,
1.74508795367418));
#92627=CARTESIAN_POINT('Ctrl Pts',(-6.68043184272131,-6.78603609293816,
1.73984128818269));
#92628=CARTESIAN_POINT('Ctrl Pts',(-7.17025078878727,-6.27146207578129,
1.72800750827385));
#92629=CARTESIAN_POINT('Ctrl Pts',(-7.42818869754932,-5.96370246256312,
1.72150523835751));
#92630=CARTESIAN_POINT('Ctrl Pts',(-7.84545710683259,-5.39660659396451,
1.71012506182612));
#92631=CARTESIAN_POINT('Ctrl Pts',(-8.01322645576272,-5.1441967112806,1.70524014268924));
#92632=CARTESIAN_POINT('Ctrl Pts',(-8.25947253865058,-4.73235941888736,
1.69726976680273));
#92633=CARTESIAN_POINT('Ctrl Pts',(-8.34601916679679,-4.57799901935649,
1.694271466573));
#92634=CARTESIAN_POINT('Ctrl Pts',(-8.59167244494509,-4.10971828127492,
1.68521694419208));
#92635=CARTESIAN_POINT('Ctrl Pts',(-8.73772708440675,-3.78929360163275,
1.67909316854293));
#92636=CARTESIAN_POINT('Ctrl Pts',(-8.97764848396376,-3.17480262877663,
1.66776322766917));
#92637=CARTESIAN_POINT('Ctrl Pts',(-9.07561965533232,-2.88282391581456,
1.66254313663657));
#92638=CARTESIAN_POINT('Ctrl Pts',(-9.2630694192839,-2.21905841259104,1.65105645539985));
#92639=CARTESIAN_POINT('Ctrl Pts',(-9.34464928971266,-1.84559107399456,
1.64485678250202));
#92640=CARTESIAN_POINT('Ctrl Pts',(-9.45249982852046,-1.15484249598211,
1.63355507572099));
#92641=CARTESIAN_POINT('Ctrl Pts',(-9.48573401283639,-0.839203371475859,
1.62844777237369));
#92642=CARTESIAN_POINT('Ctrl Pts',(-9.51271184691391,-0.34853247812069,
1.6202903080208));
#92643=CARTESIAN_POINT('Ctrl Pts',(-9.51749788160196,-0.174339772736851,
1.61734085559278));
#92644=CARTESIAN_POINT('Ctrl Pts',(-9.51749999976682,-7.71235715145945E-5,
1.61435896612853));
#92645=CARTESIAN_POINT('Ctrl Pts',(-9.5175,-3.85617845035904E-5,1.61435830627905));
#92646=CARTESIAN_POINT('Ctrl Pts',(-9.5175,4.49712710671297E-14,1.6143576464275));
#92647=CARTESIAN_POINT('Origin',(0.,0.,0.));
#92648=CARTESIAN_POINT('',(-9.51749999978858,-6.34387934023151E-5,0.614026678148392));
#92649=CARTESIAN_POINT('',(-9.5175,1.29540191486526E-8,0.886232496861817));
#92650=CARTESIAN_POINT('',(-9.5175,-1.16555759108849E-15,0.));
#92651=CARTESIAN_POINT('',(7.17753992463814,-6.25025814508694,0.));
#92652=CARTESIAN_POINT('Ctrl Pts',(-9.51749999978858,-6.34387934024261E-5,
0.614026678148392));
#92653=CARTESIAN_POINT('Ctrl Pts',(-9.51750157309347,0.235973984443455,
0.610078395618323));
#92654=CARTESIAN_POINT('Ctrl Pts',(-9.50871808344016,0.472047698466928,
0.606130113088254));
#92655=CARTESIAN_POINT('Ctrl Pts',(-9.49116749065726,0.707492695574145,
0.602181830558185));
#92656=CARTESIAN_POINT('Ctrl Pts',(-9.47361983589632,0.942898278481555,
0.598234208982472));
#92657=CARTESIAN_POINT('Ctrl Pts',(-9.44730802880415,1.17767507083165,0.594286587406759));
#92658=CARTESIAN_POINT('Ctrl Pts',(-9.41230203424797,1.41116145996537,0.590338965831046));
#92659=CARTESIAN_POINT('Ctrl Pts',(-9.37729948274158,1.64462488431054,0.586391732527623));
#92660=CARTESIAN_POINT('Ctrl Pts',(-9.33360449344291,1.87679787746023,0.582444499224199));
#92661=CARTESIAN_POINT('Ctrl Pts',(-9.28133860497358,2.10702632869812,0.578497265920775));
#92662=CARTESIAN_POINT('Ctrl Pts',(-9.22906886065934,2.33727176472719,0.574549741415577));
#92663=CARTESIAN_POINT('Ctrl Pts',(-9.16822701462845,2.56557209412563,0.570602216910379));
#92664=CARTESIAN_POINT('Ctrl Pts',(-9.09898547666434,2.79128456905625,0.566654692405182));
#92665=CARTESIAN_POINT('Ctrl Pts',(-9.0297433768793,3.01699887540188,0.56270713587005));
#92666=CARTESIAN_POINT('Ctrl Pts',(-8.95210153512587,3.24012501402205,0.558759579334919));
#92667=CARTESIAN_POINT('Ctrl Pts',(-8.86628209425272,3.46003584882203,0.554812022799787));
#92668=CARTESIAN_POINT('Ctrl Pts',(-8.7804466407393,3.67998771573614,0.550863729708904));
#92669=CARTESIAN_POINT('Ctrl Pts',(-8.686430644007,3.89672281538416,0.546915436618021));
#92670=CARTESIAN_POINT('Ctrl Pts',(-8.58450466405445,4.10963330758687,0.542967143527137));
#92671=CARTESIAN_POINT('Ctrl Pts',(-8.5616076317501,4.1574623146778,0.542080184240691));
#92672=CARTESIAN_POINT('Ctrl Pts',(-8.53831161263153,4.20509840113271,0.541193224954246));
#92673=CARTESIAN_POINT('Ctrl Pts',(-8.51461999986089,4.2525348332458,0.5403062656678));
#92674=CARTESIAN_POINT('Ctrl Pts',(-8.40897578712231,4.46406051426343,0.53635119023858));
#92675=CARTESIAN_POINT('Ctrl Pts',(-8.29543000322107,4.67167836467458,0.53239611480936));
#92676=CARTESIAN_POINT('Ctrl Pts',(-8.17429717557496,4.87479968156511,0.52844103938014));
#92677=CARTESIAN_POINT('Ctrl Pts',(-8.05318442491694,5.0778873324021,0.524486619479267));
#92678=CARTESIAN_POINT('Ctrl Pts',(-7.92448728551114,5.27647969478293,0.520532199578394));
#92679=CARTESIAN_POINT('Ctrl Pts',(-7.7885652819688,5.47001435999123,0.516577779677521));
#92680=CARTESIAN_POINT('Ctrl Pts',(-7.65265713781373,5.66352929129476,0.512623762991988));
#92681=CARTESIAN_POINT('Ctrl Pts',(-7.50952576290969,5.85198732392743,0.508669746306455));
#92682=CARTESIAN_POINT('Ctrl Pts',(-7.35957346783313,6.03485580785214,0.504715729620922));
#92683=CARTESIAN_POINT('Ctrl Pts',(-7.20960990419972,6.21773803390667,0.500761415800478));
#92684=CARTESIAN_POINT('Ctrl Pts',(-7.05282457337414,6.39502965166002,0.496807101980035));
#92685=CARTESIAN_POINT('Ctrl Pts',(-6.88966024492865,6.56623087923732,0.492852788159591));
#92686=CARTESIAN_POINT('Ctrl Pts',(-6.72649717499597,6.73743078631191,0.488898504839409));
#92687=CARTESIAN_POINT('Ctrl Pts',(-6.5569554025413,6.90254019411832,0.484944221519226));
#92688=CARTESIAN_POINT('Ctrl Pts',(-6.3815152392756,7.06109548872506,0.480989938199044));
#92689=CARTESIAN_POINT('Ctrl Pts',(-6.20604053498182,7.21968200003144,0.47703487635125));
#92690=CARTESIAN_POINT('Ctrl Pts',(-6.02466532918881,7.37171163013427,0.473079814503457));
#92691=CARTESIAN_POINT('Ctrl Pts',(-5.83790471857849,7.51675959086088,0.469124752655664));
#92692=CARTESIAN_POINT('Ctrl Pts',(-5.74338319082455,7.59016990367079,0.467123053866004));
#92693=CARTESIAN_POINT('Ctrl Pts',(-5.64748273071767,7.66179251461856,0.465121355076345));
#92694=CARTESIAN_POINT('Ctrl Pts',(-5.55027320997788,7.73157639453959,0.463119656286685));
#92695=CARTESIAN_POINT('Ctrl Pts',(-5.35819783036131,7.86946170788075,0.459164518436237));
#92696=CARTESIAN_POINT('Ctrl Pts',(-5.16095366513679,8.00020602784342,0.455209380585788));
#92697=CARTESIAN_POINT('Ctrl Pts',(-4.959093428077,8.12343514909817,0.45125424273534));
#92698=CARTESIAN_POINT('Ctrl Pts',(-4.75726671610235,8.24664380437684,0.447299761756869));
#92699=CARTESIAN_POINT('Ctrl Pts',(-4.55082570383888,8.3623396052951,0.443345280778399));
#92700=CARTESIAN_POINT('Ctrl Pts',(-4.34035065611748,8.4701925852923,0.439390799799929));
#92701=CARTESIAN_POINT('Ctrl Pts',(-4.12989714982282,8.57803452689282,0.43543672354954));
#92702=CARTESIAN_POINT('Ctrl Pts',(-3.91541068393433,8.67803512147413,0.431482647299151));
#92703=CARTESIAN_POINT('Ctrl Pts',(-3.69749550318223,8.76991067536878,0.427528571048762));
#92704=CARTESIAN_POINT('Ctrl Pts',(-3.47956409399778,8.86179307135769,0.423574200333074));
#92705=CARTESIAN_POINT('Ctrl Pts',(-3.2582037191723,8.94554910533614,0.419619829617386));
#92706=CARTESIAN_POINT('Ctrl Pts',(-3.03403909481477,9.02094302282946,0.415665458901698));
#92707=CARTESIAN_POINT('Ctrl Pts',(-2.80987629130963,9.09633632791039,0.411711120306713));
#92708=CARTESIAN_POINT('Ctrl Pts',(-2.58290955247713,9.16336756440958,0.407756781711728));
#92709=CARTESIAN_POINT('Ctrl Pts',(-2.35377994774284,9.22185047632002,0.403802443116743));
#92710=CARTESIAN_POINT('Ctrl Pts',(-2.12460539387736,9.28034486102151,0.399847328785753));
#92711=CARTESIAN_POINT('Ctrl Pts',(-1.89326740023424,9.33028750035805,0.395892214454763));
#92712=CARTESIAN_POINT('Ctrl Pts',(-1.66041971099122,9.37154270295728,0.391937100123772));
#92713=CARTESIAN_POINT('Ctrl Pts',(-1.54259505823751,9.39241849492387,0.389935749051038));
#92714=CARTESIAN_POINT('Ctrl Pts',(-1.42438401416757,9.41107066063499,0.387934397978304));
#92715=CARTESIAN_POINT('Ctrl Pts',(-1.30587213655077,9.42748663287201,0.38593304690557));
#92716=CARTESIAN_POINT('Ctrl Pts',(-1.07161009624955,9.45993603142265,0.381976982795493));
#92717=CARTESIAN_POINT('Ctrl Pts',(-0.836104249548172,9.48365409010825,
0.378020918685415));
#92718=CARTESIAN_POINT('Ctrl Pts',(-0.600018338006404,9.49856748378702,
0.374064854575338));
#92719=CARTESIAN_POINT('Ctrl Pts',(-0.363971284152349,9.51347842285089,
0.370109441599006));
#92720=CARTESIAN_POINT('Ctrl Pts',(-0.127344637748537,9.51958757203093,
0.366154028622673));
#92721=CARTESIAN_POINT('Ctrl Pts',(0.109194117260377,9.51687358825133,0.362198615646341));
#92722=CARTESIAN_POINT('Ctrl Pts',(0.3457088405748,9.5141598802051,0.358243604529215));
#92723=CARTESIAN_POINT('Ctrl Pts',(0.582135408055343,9.50262483234878,0.354288593412089));
#92724=CARTESIAN_POINT('Ctrl Pts',(0.817806698357784,9.4822992177067,0.350333582294962));
#92725=CARTESIAN_POINT('Ctrl Pts',(1.05349539243161,9.46197210206572,0.346378279109552));
#92726=CARTESIAN_POINT('Ctrl Pts',(1.28842841629673,9.43285314413454,0.342422975924142));
#92727=CARTESIAN_POINT('Ctrl Pts',(1.52194289042441,9.39502507118989,0.338467672738731));
#92728=CARTESIAN_POINT('Ctrl Pts',(1.7554552913616,9.3571973340908,0.334512404669332));
#92729=CARTESIAN_POINT('Ctrl Pts',(1.98754888935041,9.31066068399785,0.330557136599934));
#92730=CARTESIAN_POINT('Ctrl Pts',(2.21756941301968,9.25554926238522,0.326601868530535));
#92731=CARTESIAN_POINT('Ctrl Pts',(2.44763444350595,9.20042717722867,0.322645835153809));
#92732=CARTESIAN_POINT('Ctrl Pts',(2.67562532348104,9.13672707109781,0.318689801777082));
#92733=CARTESIAN_POINT('Ctrl Pts',(2.90090014069909,9.06463372804947,0.314733768400356));
#92734=CARTESIAN_POINT('Ctrl Pts',(3.01454890114918,9.02826339968642,0.312737991441723));
#92735=CARTESIAN_POINT('Ctrl Pts',(3.12750662476514,8.98975770540854,0.31074221448309));
#92736=CARTESIAN_POINT('Ctrl Pts',(3.23969245632158,8.94914515685454,0.308746437524456));
#92737=CARTESIAN_POINT('Ctrl Pts',(3.46187307311825,8.86871324346383,0.304793862145678));
#92738=CARTESIAN_POINT('Ctrl Pts',(3.68109027492723,8.77999103353609,0.3008412867669));
#92739=CARTESIAN_POINT('Ctrl Pts',(3.8967236268419,8.68322239874185,0.296888711388122));
#92740=CARTESIAN_POINT('Ctrl Pts',(4.11232065731574,8.58647006372782,0.292936801784056));
#92741=CARTESIAN_POINT('Ctrl Pts',(4.32433478448108,8.48167412535776,0.288984892179989));
#92742=CARTESIAN_POINT('Ctrl Pts',(4.53216647343998,8.36912619734143,0.285032982575923));
#92743=CARTESIAN_POINT('Ctrl Pts',(4.73997681778519,8.25658982815936,0.281081478838663));
#92744=CARTESIAN_POINT('Ctrl Pts',(4.94360533247279,8.13630319390262,0.277129975101402));
#92745=CARTESIAN_POINT('Ctrl Pts',(5.14247708649228,8.0086038524141,0.273178471364142));
#92746=CARTESIAN_POINT('Ctrl Pts',(5.34136449032563,7.88089446188198,0.26922665667122));
#92747=CARTESIAN_POINT('Ctrl Pts',(5.53549414558515,7.74577134940408,0.265274841978297));
#92748=CARTESIAN_POINT('Ctrl Pts',(5.72431908569665,7.60361606442153,0.261323027285375));
#92749=CARTESIAN_POINT('Ctrl Pts',(5.91314314972675,7.46146143898956,0.257371230927485));
#92750=CARTESIAN_POINT('Ctrl Pts',(6.09666232288001,7.312274878722,0.253419434569594));
#92751=CARTESIAN_POINT('Ctrl Pts',(6.27436122760346,7.15647940230016,0.249467638211704));
#92752=CARTESIAN_POINT('Ctrl Pts',(6.45209667352698,7.00065188880031,0.245515029224261));
#92753=CARTESIAN_POINT('Ctrl Pts',(6.62400924636439,6.83821293048068,0.241562420236818));
#92754=CARTESIAN_POINT('Ctrl Pts',(6.78961811626248,6.66962458353694,0.237609811249375));
#92755=CARTESIAN_POINT('Ctrl Pts',(6.87411343469442,6.58360910581711,0.235593150214031));
#92756=CARTESIAN_POINT('Ctrl Pts',(6.95696838808337,6.49599345866659,0.233576489178686));
#92757=CARTESIAN_POINT('Ctrl Pts',(7.0381228724021,6.40684264540424,0.231559828143342));
#92758=CARTESIAN_POINT('Ctrl Pts',(7.19753392928209,6.23172446822446,0.227598518183558));
#92759=CARTESIAN_POINT('Ctrl Pts',(7.35042765725365,6.05063002888739,0.223637208223773));
#92760=CARTESIAN_POINT('Ctrl Pts',(7.49636750072117,5.8640668945819,0.219675898263989));
#92761=CARTESIAN_POINT('Ctrl Pts',(7.64228387241871,5.67753376556402,0.215715225408878));
#92762=CARTESIAN_POINT('Ctrl Pts',(7.78124841937268,5.48553391856034,0.211754552553766));
#92763=CARTESIAN_POINT('Ctrl Pts',(7.91286536696382,5.28860737191792,0.207793879698655));
#92764=CARTESIAN_POINT('Ctrl Pts',(8.04446888443175,5.0917009195554,0.203833610988492));
#92765=CARTESIAN_POINT('Ctrl Pts',(8.16872614363592,4.88986900480745,0.199873342278328));
#92766=CARTESIAN_POINT('Ctrl Pts',(8.28528457174957,4.68368079774109,0.195913073568165));
#92767=CARTESIAN_POINT('Ctrl Pts',(8.40185037767259,4.47747953956113,0.191952554184515));
#92768=CARTESIAN_POINT('Ctrl Pts',(8.51071623831146,4.26692168130982,0.187992034800864));
#92769=CARTESIAN_POINT('Ctrl Pts',(8.6115748389386,4.05260225575614,0.184031515417214));
#92770=CARTESIAN_POINT('Ctrl Pts',(8.71243170439413,3.83828651735436,0.180071064170348));
#92771=CARTESIAN_POINT('Ctrl Pts',(8.80528146745874,3.62020959599289,0.176110612923482));
#92772=CARTESIAN_POINT('Ctrl Pts',(8.88986408205819,3.39898850432475,0.172150161676617));
#92773=CARTESIAN_POINT('Ctrl Pts',(8.97446126969002,3.17772929770653,0.168189028069853));
#92774=CARTESIAN_POINT('Ctrl Pts',(9.05078836227741,2.95332510066818,0.164227894463089));
#92775=CARTESIAN_POINT('Ctrl Pts',(9.11863406808458,2.72641137438343,0.160266760856326));
#92776=CARTESIAN_POINT('Ctrl Pts',(9.15228197150256,2.61387409504633,0.158302246824959));
#92777=CARTESIAN_POINT('Ctrl Pts',(9.18384452523986,2.50071981772256,0.156337732793593));
#92778=CARTESIAN_POINT('Ctrl Pts',(9.2133005174545,2.38702740350266,0.154373218762227));
#92779=CARTESIAN_POINT('Ctrl Pts',(9.27243444618333,2.15878592820287,0.150429388526563));
#92780=CARTESIAN_POINT('Ctrl Pts',(9.3230923220925,1.92830928422966,0.146485558290898));
#92781=CARTESIAN_POINT('Ctrl Pts',(9.36512475076436,1.6962442785816,0.142541728055234));
#92782=CARTESIAN_POINT('Ctrl Pts',(9.40715003705868,1.46421870667399,0.138598567976525));
#92783=CARTESIAN_POINT('Ctrl Pts',(9.44055275076671,1.23060559304961,0.134655407897817));
#92784=CARTESIAN_POINT('Ctrl Pts',(9.46523468695665,0.996061529641996,0.130712247819109));
#92785=CARTESIAN_POINT('Ctrl Pts',(9.48991421482022,0.761540351742488,0.126769472492079));
#92786=CARTESIAN_POINT('Ctrl Pts',(9.5058746342629,0.526088689685904,0.122826697165049));
#92787=CARTESIAN_POINT('Ctrl Pts',(9.51306954646726,0.29036882421709,0.118883921838019));
#92788=CARTESIAN_POINT('Ctrl Pts',(9.5202651941705,0.0546248623183552,0.114940743461338));
#92789=CARTESIAN_POINT('Ctrl Pts',(9.51869353268557,-0.181387072038218,
0.110997565084658));
#92790=CARTESIAN_POINT('Ctrl Pts',(9.50836026040628,-0.417002887671913,
0.107054386707978));
#92791=CARTESIAN_POINT('Ctrl Pts',(9.49802686177878,-0.652621584254886,
0.103111160116805));
#92792=CARTESIAN_POINT('Ctrl Pts',(9.47893165385032,-0.887843866900617,
0.0991679335256324));
#92793=CARTESIAN_POINT('Ctrl Pts',(9.45113239905309,-1.12200830013374,0.0952247069344598));
#92794=CARTESIAN_POINT('Ctrl Pts',(9.42332632570476,-1.35623016879688,0.0912805131557782));
#92795=CARTESIAN_POINT('Ctrl Pts',(9.38681197351291,-1.5893933855905,0.0873363193770966));
#92796=CARTESIAN_POINT('Ctrl Pts',(9.34169883327627,-1.82084298015092,0.0833921255984151));
#92797=CARTESIAN_POINT('Ctrl Pts',(9.31803955594689,-1.94222513436924,0.0813236201926478));
#92798=CARTESIAN_POINT('Ctrl Pts',(9.29201611827713,-2.06313611452594,0.0792551147868806));
#92799=CARTESIAN_POINT('Ctrl Pts',(9.26364992592769,-2.18348260809652,0.0771866093811133));
#92800=CARTESIAN_POINT('Ctrl Pts',(9.20909789291053,-2.41492522858947,0.0732085930932201));
#92801=CARTESIAN_POINT('Ctrl Pts',(9.14586125259741,-2.64435153131898,0.069230576805327));
#92802=CARTESIAN_POINT('Ctrl Pts',(9.07411359320576,-2.87110932351913,0.0652525605174338));
#92803=CARTESIAN_POINT('Ctrl Pts',(9.00237828592216,-3.09782807699977,0.0612752290865439));
#92804=CARTESIAN_POINT('Ctrl Pts',(8.92213496819583,-3.32187897427633,0.0572978976556541));
#92805=CARTESIAN_POINT('Ctrl Pts',(8.83360704406796,-3.5426251341333,0.0533205662247642));
#92806=CARTESIAN_POINT('Ctrl Pts',(8.74509040743746,-3.76334314838846,0.0493437419120355));
#92807=CARTESIAN_POINT('Ctrl Pts',(8.64829137627522,-3.98075701063916,0.0453669175993068));
#92808=CARTESIAN_POINT('Ctrl Pts',(8.54348183318892,-4.19424896924001,0.0413900932865782));
#92809=CARTESIAN_POINT('Ctrl Pts',(8.43867307522417,-4.40773932858633,0.0374132987639847));
#92810=CARTESIAN_POINT('Ctrl Pts',(8.32585404456452,-4.61730759427663,0.0334365042413912));
#92811=CARTESIAN_POINT('Ctrl Pts',(8.20534354533062,-4.82235871261162,0.0294597097187977));
#92812=CARTESIAN_POINT('Ctrl Pts',(8.08484098218856,-5.02739632752143,0.025483177083814));
#92813=CARTESIAN_POINT('Ctrl Pts',(7.95664810308623,-5.22791715209812,0.0215066444488302));
#92814=CARTESIAN_POINT('Ctrl Pts',(7.82112862805113,-5.42335258244188,0.0175301118138464));
#92815=CARTESIAN_POINT('Ctrl Pts',(7.68559945771733,-5.61880199457589,0.013553294690809));
#92816=CARTESIAN_POINT('Ctrl Pts',(7.5427428007723,-5.80916505843287,0.00957647756777154));
#92817=CARTESIAN_POINT('Ctrl Pts',(7.39296521290532,-5.99390286964777,0.0055996604447341));
#92818=CARTESIAN_POINT('Ctrl Pts',(7.32266580776647,-6.08061115771684,0.00373310696315578));
#92819=CARTESIAN_POINT('Ctrl Pts',(7.250842335954,-6.16608066448073,0.00186655348157747));
#92820=CARTESIAN_POINT('Ctrl Pts',(7.17753992463814,-6.25025814508694,-8.42340928558192E-16));
#92821=CARTESIAN_POINT('',(-7.17208764054957,-6.25651381571847,0.));
#92822=CARTESIAN_POINT('Origin',(0.,0.,0.));
#92823=CARTESIAN_POINT('Ctrl Pts',(-7.17208764054957,-6.25651381571847,
-1.39027244577816E-13));
#92824=CARTESIAN_POINT('Ctrl Pts',(-6.93903462647267,-6.52367164371758,
0.0061230893854338));
#92825=CARTESIAN_POINT('Ctrl Pts',(-6.69123339070042,-6.7776024280055,0.0122580412302597));
#92826=CARTESIAN_POINT('Ctrl Pts',(-6.30452767684011,-7.1319440507319,0.0211629916357882));
#92827=CARTESIAN_POINT('Ctrl Pts',(-6.17615941472648,-7.24339356681062,
0.0240227154141973));
#92828=CARTESIAN_POINT('Ctrl Pts',(-5.7288020833808,-7.61124719676084,0.0336737688681814));
#92829=CARTESIAN_POINT('Ctrl Pts',(-5.39629636960243,-7.85049324062235,
0.040304840357762));
#92830=CARTESIAN_POINT('Ctrl Pts',(-4.79736821589071,-8.22535628963563,
0.0517290676460848));
#92831=CARTESIAN_POINT('Ctrl Pts',(-4.53805647802596,-8.37121672575455,
0.0565290406610172));
#92832=CARTESIAN_POINT('Ctrl Pts',(-4.11474818325647,-8.58386614549834,
0.0644019772056237));
#92833=CARTESIAN_POINT('Ctrl Pts',(-3.95498339006568,-8.65863821250177,
0.0673918993382834));
#92834=CARTESIAN_POINT('Ctrl Pts',(-3.47181792969002,-8.86860217795716,
0.0764142496008092));
#92835=CARTESIAN_POINT('Ctrl Pts',(-3.1429312215907,-8.99041759378516,0.0825128523844614));
#92836=CARTESIAN_POINT('Ctrl Pts',(-2.51460321804215,-9.18443879372131,
0.0938065623632663));
#92837=CARTESIAN_POINT('Ctrl Pts',(-2.21691375716944,-9.26080128867718,
0.0990152614899264));
#92838=CARTESIAN_POINT('Ctrl Pts',(-1.53378042111751,-9.40120358700342,
0.110629246100296));
#92839=CARTESIAN_POINT('Ctrl Pts',(-1.14703762926181,-9.45618408232794,
0.116959106760903));
#92840=CARTESIAN_POINT('Ctrl Pts',(-0.44811666409676,-9.51202640574503,
0.128290902657562));
#92841=CARTESIAN_POINT('Ctrl Pts',(-0.137195121195117,-9.52158759614352,
0.133299261341023));
#92842=CARTESIAN_POINT('Ctrl Pts',(0.348202834178003,-9.51273071377279,
0.141359313310886));
#92843=CARTESIAN_POINT('Ctrl Pts',(0.522649299077872,-9.50474235636138,
0.14431573135038));
#92844=CARTESIAN_POINT('Ctrl Pts',(1.04948183162352,-9.46606920895727,0.153356122087019));
#92845=CARTESIAN_POINT('Ctrl Pts',(1.40047109956027,-9.42053925790094,0.159511759865588));
#92846=CARTESIAN_POINT('Ctrl Pts',(2.0521469596991,-9.29877219378344,0.170900693840379));
#92847=CARTESIAN_POINT('Ctrl Pts',(2.35323402853859,-9.22717524016697,0.176147835831803));
#92848=CARTESIAN_POINT('Ctrl Pts',(3.03168093204356,-9.03047034069168,0.18791434374575));
#92849=CARTESIAN_POINT('Ctrl Pts',(3.40576693954906,-8.89613606310804,0.194353012662929));
#92850=CARTESIAN_POINT('Ctrl Pts',(4.05117081013989,-8.61767658636625,0.205715393491159));
#92851=CARTESIAN_POINT('Ctrl Pts',(4.3259700327581,-8.48306053270267,0.210646029435909));
#92852=CARTESIAN_POINT('Ctrl Pts',(4.74852512589343,-8.25018320678865,0.218659539627829));
#92853=CARTESIAN_POINT('Ctrl Pts',(4.90083559481307,-8.16062638286779,0.221652710352832));
#92854=CARTESIAN_POINT('Ctrl Pts',(5.3488746056791,-7.88011538115239,0.230703101108145));
#92855=CARTESIAN_POINT('Ctrl Pts',(5.63659598376065,-7.67694369687641,0.236828327815319));
#92856=CARTESIAN_POINT('Ctrl Pts',(6.15383059494878,-7.26691760843837,0.248165056450992));
#92857=CARTESIAN_POINT('Ctrl Pts',(6.38582419056159,-7.0639205655047,0.253390331038366));
#92858=CARTESIAN_POINT('Ctrl Pts',(6.88594454724076,-6.58150257688345,0.264963075984794));
#92859=CARTESIAN_POINT('Ctrl Pts',(7.14769691895456,-6.29625592632983,0.271239177315086));
#92860=CARTESIAN_POINT('Ctrl Pts',(7.58889963078379,-5.75236682723046,0.282559928318293));
#92861=CARTESIAN_POINT('Ctrl Pts',(7.77427785843031,-5.49924753245593,0.287610598788987));
#92862=CARTESIAN_POINT('Ctrl Pts',(8.04300668964976,-5.09150268042808,0.295718146938713));
#92863=CARTESIAN_POINT('Ctrl Pts',(8.13515071825344,-4.9429422055558,0.298677714877409));
#92864=CARTESIAN_POINT('Ctrl Pts',(8.40099810587543,-4.48673708245598,0.307714144528223));
#92865=CARTESIAN_POINT('Ctrl Pts',(8.56171720086413,-4.17187945843736,0.313862251834349));
#92866=CARTESIAN_POINT('Ctrl Pts',(8.82963434257283,-3.56595280291705,0.325243688844295));
#92867=CARTESIAN_POINT('Ctrl Pts',(8.9408444187103,-3.27715805945244,0.330490642303489));
#92868=CARTESIAN_POINT('Ctrl Pts',(9.16382244088416,-2.60169089969545,0.342339346020211));
#92869=CARTESIAN_POINT('Ctrl Pts',(9.26553193865112,-2.21231928162504,0.348855359099864));
#92870=CARTESIAN_POINT('Ctrl Pts',(9.40003846699103,-1.52099879019535,0.36023896822764));
#92871=CARTESIAN_POINT('Ctrl Pts',(9.44359705905848,-1.22173368101764,0.365113575888356));
#92872=CARTESIAN_POINT('Ctrl Pts',(9.48997557148242,-0.744664192243146,
0.37307549570592));
#92873=CARTESIAN_POINT('Ctrl Pts',(9.50218701820347,-0.567980319390919,
0.376076271696077));
#92874=CARTESIAN_POINT('Ctrl Pts',(9.52391782942472,-0.0395498460445606,
0.385132330140256));
#92875=CARTESIAN_POINT('Ctrl Pts',(9.51887201789631,0.312492190247613,0.391254949842456));
#92876=CARTESIAN_POINT('Ctrl Pts',(9.484396062492,0.805866170593425,0.399749285239025));
#92877=CARTESIAN_POINT('Ctrl Pts',(9.47124065166592,0.948045161219863,0.402188627261551));
#92878=CARTESIAN_POINT('Ctrl Pts',(9.42341516528679,1.3629413531227,0.409272371137488));
#92879=CARTESIAN_POINT('Ctrl Pts',(9.38012353863364,1.63451710866645,0.413861802731057));
#92880=CARTESIAN_POINT('Ctrl Pts',(9.23734497894092,2.33385669724583,0.425606340552339));
#92881=CARTESIAN_POINT('Ctrl Pts',(9.1199126850069,2.75728499585502,0.432627478567698));
#92882=CARTESIAN_POINT('Ctrl Pts',(8.90643697025229,3.36138657875957,0.443044725695659));
#92883=CARTESIAN_POINT('Ctrl Pts',(8.83315617802637,3.54949167379445,0.446353177511085));
#92884=CARTESIAN_POINT('Ctrl Pts',(8.62923560964239,4.02741703509139,0.455072861877973));
#92885=CARTESIAN_POINT('Ctrl Pts',(8.4899596294393,4.31327946293116,0.460572111123676));
#92886=CARTESIAN_POINT('Ctrl Pts',(8.14767411006479,4.93473826048226,0.47283405036059));
#92887=CARTESIAN_POINT('Ctrl Pts',(7.9376999305089,5.26584831376671,0.479573883988482));
#92888=CARTESIAN_POINT('Ctrl Pts',(7.53246248753103,5.82531367544405,0.491181991726077));
#92889=CARTESIAN_POINT('Ctrl Pts',(7.34568158336914,6.05914466004674,0.496114180341433));
#92890=CARTESIAN_POINT('Ctrl Pts',(6.92143901901578,6.54174662953664,0.506581109895527));
#92891=CARTESIAN_POINT('Ctrl Pts',(6.68088222440156,6.78723647116784,0.512087080439486));
#92892=CARTESIAN_POINT('Ctrl Pts',(6.28566320240162,7.14914509421464,0.520811728326618));
#92893=CARTESIAN_POINT('Ctrl Pts',(6.13983283273638,7.27477081400398,0.523972939784433));
#92894=CARTESIAN_POINT('Ctrl Pts',(5.70965804937142,7.62319053641709,0.53327316987596));
#92895=CARTESIAN_POINT('Ctrl Pts',(5.41631201448006,7.83433420932491,0.539546928319713));
#92896=CARTESIAN_POINT('Ctrl Pts',(4.79156620939356,8.23211480678324,0.552337823888925));
#92897=CARTESIAN_POINT('Ctrl Pts',(4.45954718942792,8.41660639181572,0.558836830020347));
#92898=CARTESIAN_POINT('Ctrl Pts',(3.6171240691741,8.82083450440868,0.57447283004648));
#92899=CARTESIAN_POINT('Ctrl Pts',(3.09681563521564,9.01667563362379,0.583371743534608));
#92900=CARTESIAN_POINT('Ctrl Pts',(2.40311850818849,9.2106018729805,0.595051578877104));
#92901=CARTESIAN_POINT('Ctrl Pts',(2.24268654987239,9.25097411902166,0.597746499402488));
#92902=CARTESIAN_POINT('Ctrl Pts',(1.92204906354856,9.32283020852283,0.603179909631795));
#92903=CARTESIAN_POINT('Ctrl Pts',(1.76192419563051,9.35441382094635,0.605925368279426));
#92904=CARTESIAN_POINT('Ctrl Pts',(1.19689896788042,9.45083850133323,0.615694606522176));
#92905=CARTESIAN_POINT('Ctrl Pts',(0.788695762157428,9.49362292415194,0.62284887419601));
#92906=CARTESIAN_POINT('Ctrl Pts',(0.240331629698746,9.51547731476212,0.632261001700232));
#92907=CARTESIAN_POINT('Ctrl Pts',(0.101551135275765,9.5179701267666,0.634628281815932));
#92908=CARTESIAN_POINT('Ctrl Pts',(-0.313076632471723,9.5163480064041,0.641649272785042));
#92909=CARTESIAN_POINT('Ctrl Pts',(-0.588742290031258,9.50327733658267,
0.646245392585186));
#92910=CARTESIAN_POINT('Ctrl Pts',(-1.29686298829185,9.43876883670776,0.657925204241282));
#92911=CARTESIAN_POINT('Ctrl Pts',(-1.72705398894358,9.36960477193262,0.664882384171149));
#92912=CARTESIAN_POINT('Ctrl Pts',(-2.33948415145625,9.22751643348909,0.675116364779935));
#92913=CARTESIAN_POINT('Ctrl Pts',(-2.52659310716908,9.17804843189477,0.678294144464204));
#92914=CARTESIAN_POINT('Ctrl Pts',(-3.06181965502673,9.01893600376006,0.687673717547856));
#92915=CARTESIAN_POINT('Ctrl Pts',(-3.40530615496613,8.89493314214931,0.694014113124501));
#92916=CARTESIAN_POINT('Ctrl Pts',(-4.08749631636078,8.60333201070961,0.706825838192722));
#92917=CARTESIAN_POINT('Ctrl Pts',(-4.42506069933576,8.43467776045108,0.713280882380909));
#92918=CARTESIAN_POINT('Ctrl Pts',(-5.24141516659108,7.96428153648384,0.729046276778006));
#92919=CARTESIAN_POINT('Ctrl Pts',(-5.70499077821504,7.63906352539674,0.738098833647876));
#92920=CARTESIAN_POINT('Ctrl Pts',(-6.30478761351065,7.13306853728811,0.750832383610307));
#92921=CARTESIAN_POINT('Ctrl Pts',(-6.46765868318376,6.98572861633838,0.754419700370793));
#92922=CARTESIAN_POINT('Ctrl Pts',(-6.87325735196992,6.5924531042719,0.76388476937299));
#92923=CARTESIAN_POINT('Ctrl Pts',(-7.10795440520615,6.33869763974769,0.769872491752266));
#92924=CARTESIAN_POINT('Ctrl Pts',(-7.58547631657443,5.76244433440629,0.782804768294171));
#92925=CARTESIAN_POINT('Ctrl Pts',(-7.822648572792,5.43611892772742,0.789722275950427));
#92926=CARTESIAN_POINT('Ctrl Pts',(-8.34470945056656,4.61257954687358,0.806049318590966));
#92927=CARTESIAN_POINT('Ctrl Pts',(-8.60681087485979,4.10278811277121,0.815211938072408));
#92928=CARTESIAN_POINT('Ctrl Pts',(-8.90373927600287,3.36959661091949,0.828048651279066));
#92929=CARTESIAN_POINT('Ctrl Pts',(-8.97890475680381,3.1638620915177,0.831626665530576));
#92930=CARTESIAN_POINT('Ctrl Pts',(-9.15392422270132,2.62816006554718,0.841068894646166));
#92931=CARTESIAN_POINT('Ctrl Pts',(-9.24307231355284,2.29503099039305,0.847042466013865));
#92932=CARTESIAN_POINT('Ctrl Pts',(-9.39664789694852,1.5644182744876,0.859943462994976));
#92933=CARTESIAN_POINT('Ctrl Pts',(-9.454332849096,1.16618635295279,0.866844176838761));
#92934=CARTESIAN_POINT('Ctrl Pts',(-9.50721563147286,0.510823228395225,
0.877855553603315));
#92935=CARTESIAN_POINT('Ctrl Pts',(-9.51749999965232,0.255449492998535,
0.882066736325325));
#92936=CARTESIAN_POINT('Ctrl Pts',(-9.5175,1.29540203563927E-8,0.886232496861817));
#92937=CARTESIAN_POINT('Origin',(0.,0.,0.));
#92938=CARTESIAN_POINT('Ctrl Pts',(-9.5175,1.29540191486526E-8,0.886232496861817));
#92939=CARTESIAN_POINT('Ctrl Pts',(-9.51750000009661,-0.0709834321008029,
0.887390064432916));
#92940=CARTESIAN_POINT('Ctrl Pts',(-9.51670588696209,-0.141972721806853,
0.888544370346134));
#92941=CARTESIAN_POINT('Ctrl Pts',(-9.50834368299895,-0.515608100225471,
0.894608759845094));
#92942=CARTESIAN_POINT('Ctrl Pts',(-9.48713394327634,-0.817765315791146,
0.899469037072768));
#92943=CARTESIAN_POINT('Ctrl Pts',(-9.4300283608135,-1.30036435445735,0.907393967643415));
#92944=CARTESIAN_POINT('Ctrl Pts',(-9.40324558456404,-1.48167305946214,
0.910411653856429));
#92945=CARTESIAN_POINT('Ctrl Pts',(-9.32253051541496,-1.93676161781098,
0.918187617085166));
#92946=CARTESIAN_POINT('Ctrl Pts',(-9.26176363468904,-2.20915240447229,
0.923003836304866));
#92947=CARTESIAN_POINT('Ctrl Pts',(-9.1108138684556,-2.76880843345181,0.933021129377397));
#92948=CARTESIAN_POINT('Ctrl Pts',(-9.01879084958096,-3.05526468133464,
0.938215956004931));
#92949=CARTESIAN_POINT('Ctrl Pts',(-8.81658594895157,-3.59538706373471,
0.948028533439706));
#92950=CARTESIAN_POINT('Ctrl Pts',(-8.7086102079461,-3.84955912891823,0.952654765272702));
#92951=CARTESIAN_POINT('Ctrl Pts',(-8.53013525825724,-4.22359508010476,
0.959495498211941));
#92952=CARTESIAN_POINT('Ctrl Pts',(-8.46781261296457,-4.34719594757657,
0.9617625407189));
#92953=CARTESIAN_POINT('Ctrl Pts',(-8.21187337611752,-4.82838211024614,
0.970641832374481));
#92954=CARTESIAN_POINT('Ctrl Pts',(-7.99812237261707,-5.1747631784986,0.977134414953339));
#92955=CARTESIAN_POINT('Ctrl Pts',(-7.66765777885033,-5.64064867599083,
0.986500687327036));
#92956=CARTESIAN_POINT('Ctrl Pts',(-7.56897356942488,-5.7723939968927,0.989233766450829));
#92957=CARTESIAN_POINT('Ctrl Pts',(-7.20619398893471,-6.2314026107354,0.999125624719866));
#92958=CARTESIAN_POINT('Ctrl Pts',(-6.9238916009016,-6.54364856002412,1.00646724688607));
#92959=CARTESIAN_POINT('Ctrl Pts',(-6.39344966556373,-7.05745974374448,
1.01916838056406));
#92960=CARTESIAN_POINT('Ctrl Pts',(-6.15408358454014,-7.26713106377084,
1.02457215942581));
#92961=CARTESIAN_POINT('Ctrl Pts',(-5.59026126480687,-7.713137863628,1.03655932876923));
#92962=CARTESIAN_POINT('Ctrl Pts',(-5.26045213186174,-7.94173543092669,
1.04306374587039));
#92963=CARTESIAN_POINT('Ctrl Pts',(-4.62927364203687,-8.32260350261557,
1.05497990239583));
#92964=CARTESIAN_POINT('Ctrl Pts',(-4.33233022242226,-8.48096783617631,
1.06039584712114));
#92965=CARTESIAN_POINT('Ctrl Pts',(-3.83450372799791,-8.71348509654136,
1.06956772537983));
#92966=CARTESIAN_POINT('Ctrl Pts',(-3.63840107148738,-8.7971744169989,1.07321030995441));
#92967=CARTESIAN_POINT('Ctrl Pts',(-2.89479862660065,-9.08539580088091,
1.0869385278474));
#92968=CARTESIAN_POINT('Ctrl Pts',(-2.33163893413568,-9.24595860678656,
1.09708550198641));
#92969=CARTESIAN_POINT('Ctrl Pts',(-1.36198023479308,-9.42812950366615,
1.11354527106545));
#92970=CARTESIAN_POINT('Ctrl Pts',(-0.962329782394407,-9.4772643269652,
1.1200743946241));
#92971=CARTESIAN_POINT('Ctrl Pts',(-0.220705783416766,-9.52103682263299,
1.13208344913632));
#92972=CARTESIAN_POINT('Ctrl Pts',(0.120189287118578,-9.52283595927135,
1.13756765893452));
#92973=CARTESIAN_POINT('Ctrl Pts',(0.676338012850338,-9.49589876290568,
1.14686460760526));
#92974=CARTESIAN_POINT('Ctrl Pts',(0.891813199580838,-9.47809022878366,
1.150560149241));
#92975=CARTESIAN_POINT('Ctrl Pts',(1.68050463678258,-9.38577189627498,1.16423315658238));
#92976=CARTESIAN_POINT('Ctrl Pts',(2.24721370120664,-9.26643699723771,1.1742650943042));
#92977=CARTESIAN_POINT('Ctrl Pts',(3.18164403407643,-8.97884963655408,1.19057989921377));
#92978=CARTESIAN_POINT('Ctrl Pts',(3.55591300970609,-8.83731202866592,1.19707125070835));
#92979=CARTESIAN_POINT('Ctrl Pts',(4.23647968674317,-8.52968570655022,1.2091447559891));
#92980=CARTESIAN_POINT('Ctrl Pts',(4.54472595273265,-8.36951379449738,1.21473009194926));
#92981=CARTESIAN_POINT('Ctrl Pts',(5.03363069834457,-8.08047876267821,1.22421674216097));
#92982=CARTESIAN_POINT('Ctrl Pts',(5.2197612553087,-7.96151155746337,1.22799519729326));
#92983=CARTESIAN_POINT('Ctrl Pts',(5.86946345419365,-7.51366309695892,1.24158810181947));
#92984=CARTESIAN_POINT('Ctrl Pts',(6.30752619709711,-7.14988537595363,1.25144708784685));
#92985=CARTESIAN_POINT('Ctrl Pts',(6.99884823637462,-6.46252678755998,1.26772109283909));
#92986=CARTESIAN_POINT('Ctrl Pts',(7.26851519100125,-6.15766333443829,1.27432224142334));
#92987=CARTESIAN_POINT('Ctrl Pts',(7.72771518166854,-5.5661775759193,1.28642676817886));
#92988=CARTESIAN_POINT('Ctrl Pts',(7.92283889302851,-5.28474554875495,1.2919353148367));
#92989=CARTESIAN_POINT('Ctrl Pts',(8.2163607199155,-4.80847373089049,1.30127742306168));
#92990=CARTESIAN_POINT('Ctrl Pts',(8.32397498198234,-4.61967989770632,1.30499241947281));
#92991=CARTESIAN_POINT('Ctrl Pts',(8.69280250666164,-3.91782220788186,1.31864595980406));
#92992=CARTESIAN_POINT('Ctrl Pts',(8.91379728922954,-3.38502260911586,1.32863655767747));
#92993=CARTESIAN_POINT('Ctrl Pts',(9.20512044025394,-2.45159674083597,1.34495527392816));
#92994=CARTESIAN_POINT('Ctrl Pts',(9.30048909355446,-2.06045460944007,1.3514856796273));
#92995=CARTESIAN_POINT('Ctrl Pts',(9.43113728749645,-1.32490888918622,1.36356210594341));
#92996=CARTESIAN_POINT('Ctrl Pts',(9.47294779987285,-0.98233950570191,1.3691120887308));
#92997=CARTESIAN_POINT('Ctrl Pts',(9.51077182367394,-0.419592301126781,
1.37853180592365));
#92998=CARTESIAN_POINT('Ctrl Pts',(9.51791174868415,-0.200482182594715,
1.38228065357111));
#92999=CARTESIAN_POINT('Ctrl Pts',(9.5163598494172,0.590341328961604,1.39590131545597));
#93000=CARTESIAN_POINT('Ctrl Pts',(9.46373474772706,1.16075227234511,1.40582110477999));
#93001=CARTESIAN_POINT('Ctrl Pts',(9.2873062968508,2.11921343781519,1.42208777159612));
#93002=CARTESIAN_POINT('Ctrl Pts',(9.18928490171559,2.5104120253562,1.42862995167621));
#93003=CARTESIAN_POINT('Ctrl Pts',(8.9616333863762,3.22357935857759,1.44073171797963));
#93004=CARTESIAN_POINT('Ctrl Pts',(8.83863055512849,3.54696257932293,1.44629535229075));
#93005=CARTESIAN_POINT('Ctrl Pts',(8.60909437881218,4.06381768465117,1.45574083722301));
#93006=CARTESIAN_POINT('Ctrl Pts',(8.51294908304052,4.26155099639194,1.45950103847777));
#93007=CARTESIAN_POINT('Ctrl Pts',(8.14302371815457,4.9597657913796,1.47311094827104));
#93008=CARTESIAN_POINT('Ctrl Pts',(7.83123379026358,5.43874091396667,1.48300729939254));
#93009=CARTESIAN_POINT('Ctrl Pts',(7.22026958258221,6.21487967318774,1.4994950345681));
#93010=CARTESIAN_POINT('Ctrl Pts',(6.94080315408772,6.52550959230831,1.50626438682662));
#93011=CARTESIAN_POINT('Ctrl Pts',(6.40811169889246,7.0445304849691,1.51828584179066));
#93012=CARTESIAN_POINT('Ctrl Pts',(6.16281611713813,7.26009642940727,1.52354553115818));
#93013=CARTESIAN_POINT('Ctrl Pts',(5.74478265732109,7.5909845103392,1.53243986894394));
#93014=CARTESIAN_POINT('Ctrl Pts',(5.57849042110374,7.71401431749304,1.53597000730131));
#93015=CARTESIAN_POINT('Ctrl Pts',(4.91565986945029,8.17175417268464,1.54982722161673));
#93016=CARTESIAN_POINT('Ctrl Pts',(4.39197993134727,8.46473901976796,1.5602317445063));
#93017=CARTESIAN_POINT('Ctrl Pts',(3.48825078254916,8.86376671524525,1.57670306897099));
#93018=CARTESIAN_POINT('Ctrl Pts',(3.12294022559557,8.99897215398034,1.58302319371211));
#93019=CARTESIAN_POINT('Ctrl Pts',(2.43487386643304,9.20667201160169,1.59464239024727));
#93020=CARTESIAN_POINT('Ctrl Pts',(2.11463642651796,9.28545801484259,1.59994642489134));
#93021=CARTESIAN_POINT('Ctrl Pts',(1.61089233735988,9.3819745939804,1.60847675699062));
#93022=CARTESIAN_POINT('Ctrl Pts',(1.42986599896998,9.41126469890302,1.61158999878252));
#93023=CARTESIAN_POINT('Ctrl Pts',(0.947551587933962,9.47506556934312,1.61993150954111));
#93024=CARTESIAN_POINT('Ctrl Pts',(0.645266352138142,9.50043963158541,1.62519878088986));
#93025=CARTESIAN_POINT('Ctrl Pts',(0.0163566163675249,9.5230723323936,1.63603187654348));
#93026=CARTESIAN_POINT('Ctrl Pts',(-0.309962191910088,9.51804075318925,
1.64158125982926));
#93027=CARTESIAN_POINT('Ctrl Pts',(-1.03510627631471,9.46952261383766,1.65370907829757));
#93028=CARTESIAN_POINT('Ctrl Pts',(-1.43274608035249,9.41756570862793,1.66021429049689));
#93029=CARTESIAN_POINT('Ctrl Pts',(-2.16556940359027,9.27431292046044,1.6722849408458));
#93030=CARTESIAN_POINT('Ctrl Pts',(-2.50133510045622,9.18944451473523,1.67785386858916));
#93031=CARTESIAN_POINT('Ctrl Pts',(-3.04181774660979,9.02100743667884,1.68730937198493));
#93032=CARTESIAN_POINT('Ctrl Pts',(-3.24957184120873,8.94826866024951,1.69107400291466));
#93033=CARTESIAN_POINT('Ctrl Pts',(-3.98559894776873,8.6615548823838,1.70467975429173));
#93034=CARTESIAN_POINT('Ctrl Pts',(-4.49694169379472,8.407440795952,1.71456700217436));
#93035=CARTESIAN_POINT('Ctrl Pts',(-5.3351203097085,7.89243978082905,1.73098817343587));
#93036=CARTESIAN_POINT('Ctrl Pts',(-5.67325707085544,7.65299093832427,1.73770301967802));
#93037=CARTESIAN_POINT('Ctrl Pts',(-6.25216992893393,7.18352527932954,1.74975070899744));
#93038=CARTESIAN_POINT('Ctrl Pts',(-6.49852477355208,6.96145367325152,1.75509057393998));
#93039=CARTESIAN_POINT('Ctrl Pts',(-6.88120304579825,6.57844523581017,1.76412584499518));
#93040=CARTESIAN_POINT('Ctrl Pts',(-7.02465856119573,6.42503446352992,1.76771220481145));
#93041=CARTESIAN_POINT('Ctrl Pts',(-7.55234717807932,5.82190884061152,1.78150281214749));
#93042=CARTESIAN_POINT('Ctrl Pts',(-7.89944596455147,5.34147351644425,1.7917761810398));
#93043=CARTESIAN_POINT('Ctrl Pts',(-8.40286584019894,4.48718015892417,1.80831405038249));
#93044=CARTESIAN_POINT('Ctrl Pts',(-8.58408122184459,4.12995051875902,1.81480864133918));
#93045=CARTESIAN_POINT('Ctrl Pts',(-8.87670376182314,3.45001158098685,1.82677429801291));
#93046=CARTESIAN_POINT('Ctrl Pts',(-8.99429601809596,3.1306685694704,1.83224922210518));
#93047=CARTESIAN_POINT('Ctrl Pts',(-9.15814142220127,2.59957548864125,1.84152901497371));
#93048=CARTESIAN_POINT('Ctrl Pts',(-9.21471084429669,2.39132804659979,1.845217208863));
#93049=CARTESIAN_POINT('Ctrl Pts',(-9.37556316853414,1.70818806618257,1.85730125071232));
#93050=CARTESIAN_POINT('Ctrl Pts',(-9.45056093730129,1.2271902920474,1.86574950853255));
#93051=CARTESIAN_POINT('Ctrl Pts',(-9.50782497638863,0.495479466538355,
1.87812526961015));
#93052=CARTESIAN_POINT('Ctrl Pts',(-9.51750331214565,0.247723883817967,
1.88224283254318));
#93053=CARTESIAN_POINT('Ctrl Pts',(-9.51749999914974,-0.000127219278908824,
1.88630958681444));
#93054=CARTESIAN_POINT('Ctrl Pts',(-9.5175,4.28129753871076E-14,1.6143576464275));
#93055=CARTESIAN_POINT('Ctrl Pts',(-9.5175,0.264761493468821,1.60982716935015));
#93056=CARTESIAN_POINT('Ctrl Pts',(-9.50645215077221,0.52940754234781,1.60523476644285));
#93057=CARTESIAN_POINT('Ctrl Pts',(-9.45622299125277,1.1299673470939,1.59483331464208));
#93058=CARTESIAN_POINT('Ctrl Pts',(-9.41014897222432,1.46494985718653,1.58905042110134));
#93059=CARTESIAN_POINT('Ctrl Pts',(-9.28756606562341,2.10259528478863,1.57815890498963));
#93060=CARTESIAN_POINT('Ctrl Pts',(-9.21379885947898,2.40534870654743,1.57303816255892));
#93061=CARTESIAN_POINT('Ctrl Pts',(-9.02445704727179,3.04434376581629,1.56220410346681));
#93062=CARTESIAN_POINT('Ctrl Pts',(-8.90462410263793,3.37883442441522,1.55651873363559));
#93063=CARTESIAN_POINT('Ctrl Pts',(-8.69937575696479,3.86436089007564,1.54789936944457));
#93064=CARTESIAN_POINT('Ctrl Pts',(-8.62807894391787,4.02102942210529,1.54505365113255));
#93065=CARTESIAN_POINT('Ctrl Pts',(-8.35010441820943,4.59037334156988,1.53436890401086));
#93066=CARTESIAN_POINT('Ctrl Pts',(-8.11774221915953,4.98979305431516,1.52629305526653));
#93067=CARTESIAN_POINT('Ctrl Pts',(-7.68513605518206,5.62268586176387,1.51313169187247));
#93068=CARTESIAN_POINT('Ctrl Pts',(-7.50093240933939,5.86616802154874,1.50795966199409));
#93069=CARTESIAN_POINT('Ctrl Pts',(-7.06613244881998,6.38685125320868,1.4966666137911));
#93070=CARTESIAN_POINT('Ctrl Pts',(-6.81027080041151,6.65900215906905,1.49060605364395));
#93071=CARTESIAN_POINT('Ctrl Pts',(-6.29712230193908,7.14422527189098,1.47918850938335));
#93072=CARTESIAN_POINT('Ctrl Pts',(-6.04331432663649,7.36016666724828,1.47383042745737));
#93073=CARTESIAN_POINT('Ctrl Pts',(-5.6322595852246,7.67427073357231,1.46522512280138));
#93074=CARTESIAN_POINT('Ctrl Pts',(-5.48258691858798,7.7819032765208,1.46209448304978));
#93075=CARTESIAN_POINT('Ctrl Pts',(-5.07523783550537,8.05724767519826,1.45366293975163));
#93076=CARTESIAN_POINT('Ctrl Pts',(-4.8124017716518,8.21693791717208,1.44832219459679));
#93077=CARTESIAN_POINT('Ctrl Pts',(-4.2586334686578,8.51769034242477,1.43747821489138));
#93078=CARTESIAN_POINT('Ctrl Pts',(-3.96731105771364,8.65721969523227,1.43198855888441));
#93079=CARTESIAN_POINT('Ctrl Pts',(-3.2986213280283,8.93663461916127,1.4198985575001));
#93080=CARTESIAN_POINT('Ctrl Pts',(-2.91833753917993,9.06794621845669,1.41337503165388));
#93081=CARTESIAN_POINT('Ctrl Pts',(-2.20248782327214,9.26541472798439,1.40137128161269));
#93082=CARTESIAN_POINT('Ctrl Pts',(-1.86945804271425,9.33830746283857,1.39588685475002));
#93083=CARTESIAN_POINT('Ctrl Pts',(-1.31991486168347,9.42800889821091,1.38658964569432));
#93084=CARTESIAN_POINT('Ctrl Pts',(-1.10546520227142,9.45555246712023,1.38289407822976));
#93085=CARTESIAN_POINT('Ctrl Pts',(-0.314877301443695,9.52982963798949,
1.3692211811255));
#93086=CARTESIAN_POINT('Ctrl Pts',(0.264249849316982,9.53136856804752,1.35918938483596));
#93087=CARTESIAN_POINT('Ctrl Pts',(1.23865909769983,9.44503907041455,1.34286553088786));
#93088=CARTESIAN_POINT('Ctrl Pts',(1.63476269772059,9.38459333124713,1.3363655596436));
#93089=CARTESIAN_POINT('Ctrl Pts',(2.36432459889632,9.22565740458415,1.32429520373077));
#93090=CARTESIAN_POINT('Ctrl Pts',(2.69848705746629,9.13350697884167,1.31872143531038));
#93091=CARTESIAN_POINT('Ctrl Pts',(3.23571916524843,8.95329268710885,1.30925687709717));
#93092=CARTESIAN_POINT('Ctrl Pts',(3.44206362159594,8.87600840896958,1.30548830653284));
#93093=CARTESIAN_POINT('Ctrl Pts',(4.1715046915936,8.5735384260078,1.29188631534715));
#93094=CARTESIAN_POINT('Ctrl Pts',(4.67684682199093,8.30867797420584,1.2820072251757));
#93095=CARTESIAN_POINT('Ctrl Pts',(5.50126233918816,7.77741213732115,1.26563560574402));
#93096=CARTESIAN_POINT('Ctrl Pts',(5.83223738557223,7.53239906320663,1.25896018315535));
#93097=CARTESIAN_POINT('Ctrl Pts',(6.40222011234015,7.05029898061277,1.24689317110066));
#93098=CARTESIAN_POINT('Ctrl Pts',(6.64650562897295,6.82049104681496,1.24149509720949));
#93099=CARTESIAN_POINT('Ctrl Pts',(7.02495406145976,6.42479064197713,1.23235569169641));
#93100=CARTESIAN_POINT('Ctrl Pts',(7.16657105544514,6.26643218831147,1.22872670363757));
#93101=CARTESIAN_POINT('Ctrl Pts',(7.67858620869205,5.65380873401212,1.21498385977178));
#93102=CARTESIAN_POINT('Ctrl Pts',(8.01207445502674,5.17038849466746,1.20480683163048));
#93103=CARTESIAN_POINT('Ctrl Pts',(8.49231149569004,4.31502135256395,1.18844265166231));
#93104=CARTESIAN_POINT('Ctrl Pts',(8.66402535120185,3.95896832027939,1.182029016208));
#93105=CARTESIAN_POINT('Ctrl Pts',(8.93698042392705,3.28949984757043,1.17034139351991));
#93106=CARTESIAN_POINT('Ctrl Pts',(9.04504697864608,2.9795219455272,1.165061024439));
#93107=CARTESIAN_POINT('Ctrl Pts',(9.18810202132165,2.48898493300804,1.15656353112484));
#93108=CARTESIAN_POINT('Ctrl Pts',(9.23423912596728,2.31194531108307,1.15345793506077));
#93109=CARTESIAN_POINT('Ctrl Pts',(9.34280345625023,1.84001094025654,1.14515576011107));
#93110=CARTESIAN_POINT('Ctrl Pts',(9.39637539755217,1.5432907537012,1.13992055245723));
#93111=CARTESIAN_POINT('Ctrl Pts',(9.47862265951926,0.91970829998119,1.12909159986179));
#93112=CARTESIAN_POINT('Ctrl Pts',(9.50466385171467,0.592889640484698,1.12351550500536));
#93113=CARTESIAN_POINT('Ctrl Pts',(9.52501408299184,-0.136663810044939,
1.11133484460832));
#93114=CARTESIAN_POINT('Ctrl Pts',(9.51073273060235,-0.539012884039947,
1.10480407896102));
#93115=CARTESIAN_POINT('Ctrl Pts',(9.43694723227837,-1.28303735839833,1.09271763727561));
#93116=CARTESIAN_POINT('Ctrl Pts',(9.38416061643455,-1.62471051488265,1.08715805100552));
#93117=CARTESIAN_POINT('Ctrl Pts',(9.26762675434479,-2.17764310362065,1.07772026221169));
#93118=CARTESIAN_POINT('Ctrl Pts',(9.21491349662537,-2.3909000773591,1.07396348437403));
#93119=CARTESIAN_POINT('Ctrl Pts',(9.00038329897622,-3.14566184874142,1.06044851978369));
#93120=CARTESIAN_POINT('Ctrl Pts',(8.79779626617351,-3.67435460839335,1.05064288044717));
#93121=CARTESIAN_POINT('Ctrl Pts',(8.38391734895862,-4.52048277085164,1.03491019560779));
#93122=CARTESIAN_POINT('Ctrl Pts',(8.19836247541849,-4.84888534068094,1.02877269366243));
#93123=CARTESIAN_POINT('Ctrl Pts',(7.79566940206617,-5.47207912857135,1.01677089600701));
#93124=CARTESIAN_POINT('Ctrl Pts',(7.5800333126896,-5.76707923219049,1.01091158062097));
#93125=CARTESIAN_POINT('Ctrl Pts',(7.2249739602744,-6.19838841220579,1.00160584477148));
#93126=CARTESIAN_POINT('Ctrl Pts',(7.09743288508585,-6.34402968623607,0.998310764385156));
#93127=CARTESIAN_POINT('Ctrl Pts',(6.66895602783513,-6.80420866893346,0.987512098119311));
#93128=CARTESIAN_POINT('Ctrl Pts',(6.35086776959386,-7.10202171304785,0.979931314721207));
#93129=CARTESIAN_POINT('Ctrl Pts',(5.7997222059246,-7.55129863768712,0.967835529235672));
#93130=CARTESIAN_POINT('Ctrl Pts',(5.57844989191139,-7.71620288040075,0.963213636922584));
#93131=CARTESIAN_POINT('Ctrl Pts',(5.23552847678581,-7.9492965527016,0.956370800280709));
#93132=CARTESIAN_POINT('Ctrl Pts',(5.11903587400575,-8.02480815752726,0.954097640522328));
#93133=CARTESIAN_POINT('Ctrl Pts',(4.65190413314435,-8.31329522290424,0.945154462255196));
#93134=CARTESIAN_POINT('Ctrl Pts',(4.28930622862586,-8.50605306174694,0.938605970301876));
#93135=CARTESIAN_POINT('Ctrl Pts',(3.76674501507339,-8.74191289695796,0.929197005362934));
#93136=CARTESIAN_POINT('Ctrl Pts',(3.61638438658702,-8.80517876324774,0.926485078033962));
#93137=CARTESIAN_POINT('Ctrl Pts',(3.05140223158275,-9.0259868013857,0.916221382627433));
#93138=CARTESIAN_POINT('Ctrl Pts',(2.62755500426413,-9.15835410790396,0.908468029780455));
#93139=CARTESIAN_POINT('Ctrl Pts',(1.89931565720075,-9.33104462015247,0.895619263562257));
#93140=CARTESIAN_POINT('Ctrl Pts',(1.59939445150892,-9.387104603334,0.890450771772977));
#93141=CARTESIAN_POINT('Ctrl Pts',(0.927005229180607,-9.47961924549221,
0.879151891938266));
#93142=CARTESIAN_POINT('Ctrl Pts',(0.554031379839827,-9.50871023728457,
0.873082597931436));
#93143=CARTESIAN_POINT('Ctrl Pts',(-0.151533636219758,-9.5220799272509,
0.861673920852244));
#93144=CARTESIAN_POINT('Ctrl Pts',(-0.483481035362257,-9.51100478918671,
0.856333179038857));
#93145=CARTESIAN_POINT('Ctrl Pts',(-0.997464084631463,-9.46687471710456,
0.847752516089616));
#93146=CARTESIAN_POINT('Ctrl Pts',(-1.18026368524024,-9.44582594283233,
0.844628058884999));
#93147=CARTESIAN_POINT('Ctrl Pts',(-1.66507118868918,-9.37570848981499,
0.836228332183765));
#93148=CARTESIAN_POINT('Ctrl Pts',(-1.96551933731419,-9.31735508734775,
0.830913511219793));
#93149=CARTESIAN_POINT('Ctrl Pts',(-2.57730521635309,-9.16761980296353,
0.820073723258781));
#93150=CARTESIAN_POINT('Ctrl Pts',(-2.88783927625287,-9.07458767418222,
0.814563355697036));
#93151=CARTESIAN_POINT('Ctrl Pts',(-3.56973830841872,-8.83174310080167,
0.802486489628474));
#93152=CARTESIAN_POINT('Ctrl Pts',(-3.93762183158052,-8.67397565987705,
0.795993969897333));
#93153=CARTESIAN_POINT('Ctrl Pts',(-4.60216739881697,-8.33796906248207,
0.783956301026481));
#93154=CARTESIAN_POINT('Ctrl Pts',(-4.90116241004204,-8.16579920828296,
0.77840771084053));
#93155=CARTESIAN_POINT('Ctrl Pts',(-5.37386692839181,-7.85826929007571,
0.768989382474449));
#93156=CARTESIAN_POINT('Ctrl Pts',(-5.5533964324459,-7.7324400316803,0.765240411931296));
#93157=CARTESIAN_POINT('Ctrl Pts',(-6.18494761952274,-7.25644792347482,
0.751619593183426));
#93158=CARTESIAN_POINT('Ctrl Pts',(-6.6095536186583,-6.87193044407949,0.741699786648745));
#93159=CARTESIAN_POINT('Ctrl Pts',(-7.28716879695542,-6.13702774236959,
0.725014942153507));
#93160=CARTESIAN_POINT('Ctrl Pts',(-7.55570764647677,-5.80320800478434,
0.718081456810211));
#93161=CARTESIAN_POINT('Ctrl Pts',(-7.9734895773645,-5.20548378812184,0.706294202698439));
#93162=CARTESIAN_POINT('Ctrl Pts',(-8.13428214553769,-4.95045942633501,
0.701431470414448));
#93163=CARTESIAN_POINT('Ctrl Pts',(-8.37356853475163,-4.52771261325523,
0.693350862669414));
#93164=CARTESIAN_POINT('Ctrl Pts',(-8.45974468860711,-4.36457900772039,
0.690217683334457));
#93165=CARTESIAN_POINT('Ctrl Pts',(-8.67700828290358,-3.92265114541777,
0.68177272119757));
#93166=CARTESIAN_POINT('Ctrl Pts',(-8.79939504543731,-3.63982306623629,
0.67642097272025));
#93167=CARTESIAN_POINT('Ctrl Pts',(-9.02134429858824,-3.04992120864695,
0.665575716783025));
#93168=CARTESIAN_POINT('Ctrl Pts',(-9.1194412350741,-2.74271142732486,0.660095335448847));
#93169=CARTESIAN_POINT('Ctrl Pts',(-9.2659594934796,-2.18814063947224,0.650526801736613));
#93170=CARTESIAN_POINT('Ctrl Pts',(-9.32050527252575,-1.94271640788156,
0.646399466767897));
#93171=CARTESIAN_POINT('Ctrl Pts',(-9.44720738662408,-1.24283118030191,
0.634827590642327));
#93172=CARTESIAN_POINT('Ctrl Pts',(-9.49622449932472,-0.784901646146257,
0.62751102293297));
#93173=CARTESIAN_POINT('Ctrl Pts',(-9.5156462769228,-0.216878343335995,
0.618080772081449));
#93174=CARTESIAN_POINT('Ctrl Pts',(-9.51749935373479,-0.10847143398478,
0.616260847688148));
#93175=CARTESIAN_POINT('Ctrl Pts',(-9.51749999983099,-5.67194278485892E-5,
0.614423068612269));
#93176=CARTESIAN_POINT('Origin',(0.,0.,-2.20842344717745));
#93177=CARTESIAN_POINT('',(-10.0766107346517,-0.000128399830713298,1.29157655282254));
#93178=CARTESIAN_POINT('Ctrl Pts',(6.13570130491008,-7.99149349282772,0.645787560181147));
#93179=CARTESIAN_POINT('Ctrl Pts',(6.72491755688915,-7.53931401154324,0.65751697232479));
#93180=CARTESIAN_POINT('Ctrl Pts',(8.44842283158552,-5.88942327299567,0.694975254262141));
#93181=CARTESIAN_POINT('Ctrl Pts',(10.2494764494997,-2.18403346540847,0.758162405993196));
#93182=CARTESIAN_POINT('Ctrl Pts',(10.0857330432995,2.846007611683,0.835349015374309));
#93183=CARTESIAN_POINT('Ctrl Pts',(7.5959232928945,7.21967588414949,0.912535624755426));
#93184=CARTESIAN_POINT('Ctrl Pts',(3.35427052456325,9.92827474644192,0.989722234136537));
#93185=CARTESIAN_POINT('Ctrl Pts',(-1.6609755673321,10.3471218520573,1.06690884351765));
#93186=CARTESIAN_POINT('Ctrl Pts',(-6.29315189771966,8.37961869672186,1.14409545289877));
#93187=CARTESIAN_POINT('Ctrl Pts',(-9.3792698747427,4.59561112228605,1.21898468933373));
#93188=CARTESIAN_POINT('Ctrl Pts',(-10.075640881915,1.48301858797571,1.26814505597499));
#93189=CARTESIAN_POINT('Ctrl Pts',(-10.0766107346517,-0.000128399830713298,
1.29157655282254));
#93190=CARTESIAN_POINT('Ctrl Pts',(-10.0766107346517,-0.000128399830713298,
1.29157655282254));
#93191=CARTESIAN_POINT('Ctrl Pts',(-10.076705825181,-0.145545561487931,
1.2938739257687));
#93192=CARTESIAN_POINT('Ctrl Pts',(-10.0390551969694,-1.91947760598252,
1.32190016850855));
#93193=CARTESIAN_POINT('Ctrl Pts',(-9.05094988379608,-5.28224162230782,
1.37565528104211));
#93194=CARTESIAN_POINT('Ctrl Pts',(-5.54472111010466,-8.89257207845922,
1.45284189042322));
#93195=CARTESIAN_POINT('Ctrl Pts',(-0.759716774784057,-10.4520141971627,
1.53002849980434));
#93196=CARTESIAN_POINT('Ctrl Pts',(3.37337104626303,-9.74283791843435,1.59434403545769));
#93197=CARTESIAN_POINT('Ctrl Pts',(5.48989350430804,-8.4873022126398,1.63293070131733));
#93198=CARTESIAN_POINT('Ctrl Pts',(6.13568652661064,-7.99147452837712,1.64578849738327));
#93199=CARTESIAN_POINT('',(-10.075999998343,-0.000182733646683074,1.20842344717745));
#93200=CARTESIAN_POINT('Ctrl Pts',(-10.07551961303,-0.000183021653669313,
1.2084234518637));
#93201=CARTESIAN_POINT('Ctrl Pts',(-10.0759095234531,-0.560797522139529,
1.21727755127508));
#93202=CARTESIAN_POINT('Ctrl Pts',(-9.89602121837179,-2.75023774228373,
1.25186052048016));
#93203=CARTESIAN_POINT('Ctrl Pts',(-8.33073300645692,-6.35772433572561,
1.31217235947894));
#93204=CARTESIAN_POINT('Ctrl Pts',(-4.40617793665544,-9.50827888762232,
1.38935896886006));
#93205=CARTESIAN_POINT('Ctrl Pts',(0.534571201485628,-10.4659450075294,
1.46654557824117));
#93206=CARTESIAN_POINT('Ctrl Pts',(4.13955618575929,-9.37633040870524,1.52430557873297));
#93207=CARTESIAN_POINT('Ctrl Pts',(5.81987160391175,-8.2353133147925,1.55633670943106));
#93208=CARTESIAN_POINT('Ctrl Pts',(6.13611323687281,-7.99203043615932,1.56263897033545));
#93209=CARTESIAN_POINT('Ctrl Pts',(6.13615379320823,-7.99208312182101,0.562637467686473));
#93210=CARTESIAN_POINT('Ctrl Pts',(6.33192762783051,-7.8417720778019,0.566535835994544));
#93211=CARTESIAN_POINT('Ctrl Pts',(6.52218751259431,-7.68425508730315,0.570434204302615));
#93212=CARTESIAN_POINT('Ctrl Pts',(6.70641049035147,-7.51996238919476,0.574332572610686));
#93213=CARTESIAN_POINT('Ctrl Pts',(6.89064675943679,-7.35565783768898,0.578231222178418));
#93214=CARTESIAN_POINT('Ctrl Pts',(7.06884504128707,-7.18457678496899,0.582129871746151));
#93215=CARTESIAN_POINT('Ctrl Pts',(7.24051686463347,-7.00718856125324,0.586028521313884));
#93216=CARTESIAN_POINT('Ctrl Pts',(7.41218583111252,-6.82980328953401,0.589927106002451));
#93217=CARTESIAN_POINT('Ctrl Pts',(7.57732836392031,-6.6461112582751,0.593825690691018));
#93218=CARTESIAN_POINT('Ctrl Pts',(7.73549362466678,-6.45661787492024,0.597724275379586));
#93219=CARTESIAN_POINT('Ctrl Pts',(7.89369145557608,-6.26708547016258,0.601623662883749));
#93220=CARTESIAN_POINT('Ctrl Pts',(8.04490896415257,-6.07174953956683,0.605523050387913));
#93221=CARTESIAN_POINT('Ctrl Pts',(8.1887354273855,-5.87114878880459,0.609422437892076));
#93222=CARTESIAN_POINT('Ctrl Pts',(8.28795976554738,-5.73275647711348,0.612112583611023));
#93223=CARTESIAN_POINT('Ctrl Pts',(8.38366719749756,-5.59185907723408,0.61480272932997));
#93224=CARTESIAN_POINT('Ctrl Pts',(8.47573470011338,-5.44864178427009,0.617492875048916));
#93225=CARTESIAN_POINT('Ctrl Pts',(8.60917882552726,-5.24106032652736,0.6213920157066));
#93226=CARTESIAN_POINT('Ctrl Pts',(8.73501259619979,-5.02854433367632,0.625291156364284));
#93227=CARTESIAN_POINT('Ctrl Pts',(8.85288535627763,-4.81167298022268,0.629190297021968));
#93228=CARTESIAN_POINT('Ctrl Pts',(8.97073876951656,-4.5948372225686,0.633088797701033));
#93229=CARTESIAN_POINT('Ctrl Pts',(9.08063364767773,-4.37364777613102,0.636987298380097));
#93230=CARTESIAN_POINT('Ctrl Pts',(9.1822648995648,-4.14870911419688,0.640885799059162));
#93231=CARTESIAN_POINT('Ctrl Pts',(9.2838857665332,-3.92379343702054,0.644783901380323));
#93232=CARTESIAN_POINT('Ctrl Pts',(9.37724457861858,-3.69512956318479,0.648682003701484));
#93233=CARTESIAN_POINT('Ctrl Pts',(9.46208363779331,-3.46334364904843,0.652580106022644));
#93234=CARTESIAN_POINT('Ctrl Pts',(9.5469290019391,-3.23154050931465,0.656478498038464));
#93235=CARTESIAN_POINT('Ctrl Pts',(9.62325324959217,-2.99661512640118,0.660376890054283));
#93236=CARTESIAN_POINT('Ctrl Pts',(9.69084754622438,-2.75921181423914,0.664275282070102));
#93237=CARTESIAN_POINT('Ctrl Pts',(9.75844109264562,-2.52181113695281,0.668173630818714));
#93238=CARTESIAN_POINT('Ctrl Pts',(9.81730480755064,-2.28193285402501,0.672071979567326));
#93239=CARTESIAN_POINT('Ctrl Pts',(9.86728006718831,-2.04023529909375,0.675970328315938));
#93240=CARTESIAN_POINT('Ctrl Pts',(9.91726533662121,-1.79848933334785,0.679869457884359));
#93241=CARTESIAN_POINT('Ctrl Pts',(9.9583585364723,-1.55492364035389,0.683768587452779));
#93242=CARTESIAN_POINT('Ctrl Pts',(9.99045213222051,-1.31020692785933,0.6876677170212));
#93243=CARTESIAN_POINT('Ctrl Pts',(10.0096900009765,-1.16351635338152,0.690004972824143));
#93244=CARTESIAN_POINT('Ctrl Pts',(10.0256951503675,-1.01641237119571,0.692342228627085));
#93245=CARTESIAN_POINT('Ctrl Pts',(10.0384533319705,-0.869040103707079,
0.694679484430028));
#93246=CARTESIAN_POINT('Ctrl Pts',(10.0597380023151,-0.623176686093138,
0.698578764188304));
#93247=CARTESIAN_POINT('Ctrl Pts',(10.0719888081203,-0.376495669821744,
0.702478043946578));
#93248=CARTESIAN_POINT('Ctrl Pts',(10.0751655531142,-0.129672963032486,
0.706377323704853));
#93249=CARTESIAN_POINT('Ctrl Pts',(10.0783417780477,0.117109336767591,0.710275965117666));
#93250=CARTESIAN_POINT('Ctrl Pts',(10.0724469041336,0.364033002303638,0.714174606530479));
#93251=CARTESIAN_POINT('Ctrl Pts',(10.0574928395634,0.61042098762322,0.718073247943291));
#93252=CARTESIAN_POINT('Ctrl Pts',(10.0425402983381,0.856783873821194,0.721971492208187));
#93253=CARTESIAN_POINT('Ctrl Pts',(10.0185304260666,1.10261091075286,0.725869736473084));
#93254=CARTESIAN_POINT('Ctrl Pts',(9.98552716731234,1.34722796544131,0.72976798073798));
#93255=CARTESIAN_POINT('Ctrl Pts',(9.95252144897754,1.59186325031002,0.733666515521032));
#93256=CARTESIAN_POINT('Ctrl Pts',(9.9105210393986,1.83528809624206,0.737565050304084));
#93257=CARTESIAN_POINT('Ctrl Pts',(9.85964157667784,2.076835087205,0.741463585087136));
#93258=CARTESIAN_POINT('Ctrl Pts',(9.8087626756148,2.31837941173388,0.745362076834313));
#93259=CARTESIAN_POINT('Ctrl Pts',(9.7490049769451,2.55804565053755,0.749260568581491));
#93260=CARTESIAN_POINT('Ctrl Pts',(9.68053507517198,2.7951773930048,0.753159060328668));
#93261=CARTESIAN_POINT('Ctrl Pts',(9.61205146960001,3.03235659582491,0.757058332333234));
#93262=CARTESIAN_POINT('Ctrl Pts',(9.53485225355829,3.26700002080037,0.7609576043378));
#93263=CARTESIAN_POINT('Ctrl Pts',(9.4491540555673,3.49846589724069,0.764856876342365));
#93264=CARTESIAN_POINT('Ctrl Pts',(9.39780452966456,3.6371579969173,0.767193282165289));
#93265=CARTESIAN_POINT('Ctrl Pts',(9.34340457618121,3.77470957192005,0.769529687988214));
#93266=CARTESIAN_POINT('Ctrl Pts',(9.28600918091763,3.91098574427386,0.771866093811138));
#93267=CARTESIAN_POINT('Ctrl Pts',(9.19022230922501,4.13841632779142,0.775765309135897));
#93268=CARTESIAN_POINT('Ctrl Pts',(9.08606241920951,4.36235890696156,0.779664524460656));
#93269=CARTESIAN_POINT('Ctrl Pts',(8.97380903247485,4.58219679287925,0.783563739785414));
#93270=CARTESIAN_POINT('Ctrl Pts',(8.86157404334637,4.80199864878514,0.787462316053927));
#93271=CARTESIAN_POINT('Ctrl Pts',(8.74124833222895,5.01769690638174,0.791360892322439));
#93272=CARTESIAN_POINT('Ctrl Pts',(8.61315804758224,5.22869815990264,0.795259468590952));
#93273=CARTESIAN_POINT('Ctrl Pts',(8.48508082841011,5.43967789085827,0.799157647196603));
#93274=CARTESIAN_POINT('Ctrl Pts',(8.34924076172232,5.64596133630848,0.803055825802255));
#93275=CARTESIAN_POINT('Ctrl Pts',(8.20600867413201,5.84698192575197,0.806954004407906));
#93276=CARTESIAN_POINT('Ctrl Pts',(8.0627659234321,6.04801748044951,0.810852473218821));
#93277=CARTESIAN_POINT('Ctrl Pts',(7.91213021163992,6.24378916769073,0.814750942029737));
#93278=CARTESIAN_POINT('Ctrl Pts',(7.75451496679167,6.43376045791293,0.818649410840652));
#93279=CARTESIAN_POINT('Ctrl Pts',(7.59690146465065,6.62372964767624,0.822547836547299));
#93280=CARTESIAN_POINT('Ctrl Pts',(7.43230876335148,6.80789835558618,0.826446262253945));
#93281=CARTESIAN_POINT('Ctrl Pts',(7.26119024091035,6.98576354347242,0.830344687960591));
#93282=CARTESIAN_POINT('Ctrl Pts',(7.09003745561853,7.16366434508584,0.834243894244209));
#93283=CARTESIAN_POINT('Ctrl Pts',(6.91235643113467,7.33525890347479,0.838143100527827));
#93284=CARTESIAN_POINT('Ctrl Pts',(6.72863798502884,7.50008045733024,0.842042306811444));
#93285=CARTESIAN_POINT('Ctrl Pts',(6.61853530976719,7.59885820341359,0.844379105605051));
#93286=CARTESIAN_POINT('Ctrl Pts',(6.5062649230313,7.69520406090904,0.846715904398658));
#93287=CARTESIAN_POINT('Ctrl Pts',(6.39193840722856,7.78902429051267,0.849052703192264));
#93288=CARTESIAN_POINT('Ctrl Pts',(6.20117049557353,7.94557493099018,0.852951940588631));
#93289=CARTESIAN_POINT('Ctrl Pts',(6.00462111121729,8.09513628796777,0.856851177984997));
#93290=CARTESIAN_POINT('Ctrl Pts',(5.80282504410468,8.23729309345682,0.860750415381363));
#93291=CARTESIAN_POINT('Ctrl Pts',(5.60106203859183,8.37942660844536,0.86464901393958));
#93292=CARTESIAN_POINT('Ctrl Pts',(5.39405429405047,8.51415783336777,0.868547612497796));
#93293=CARTESIAN_POINT('Ctrl Pts',(5.18236699596795,8.64111383555975,0.872446211056012));
#93294=CARTESIAN_POINT('Ctrl Pts',(4.97070128209821,8.76805689297238,0.876344412102514));
#93295=CARTESIAN_POINT('Ctrl Pts',(4.75435720631203,8.88722616742383,0.880242613149017));
#93296=CARTESIAN_POINT('Ctrl Pts',(4.53392696973158,8.99829329557226,0.884140814195519));
#93297=CARTESIAN_POINT('Ctrl Pts',(4.31348031909844,9.10936869419084,0.888039305516524));
#93298=CARTESIAN_POINT('Ctrl Pts',(4.08894714727352,9.21234061309443,0.891937796837528));
#93299=CARTESIAN_POINT('Ctrl Pts',(3.86094333935531,9.30692712608667,0.895836288158533));
#93300=CARTESIAN_POINT('Ctrl Pts',(3.63294205227916,9.40151259331717,0.899734736377271));
#93301=CARTESIAN_POINT('Ctrl Pts',(3.40147046404377,9.48771273523951,0.903633184596009));
#93302=CARTESIAN_POINT('Ctrl Pts',(3.16716418952138,9.56529387926024,0.907531632814748));
#93303=CARTESIAN_POINT('Ctrl Pts',(2.93281100895227,9.64289055434079,0.911430861468388));
#93304=CARTESIAN_POINT('Ctrl Pts',(2.69562227260788,9.71186469568564,0.915330090122028));
#93305=CARTESIAN_POINT('Ctrl Pts',(2.45624980566499,9.77203217822018,0.919229318775668));
#93306=CARTESIAN_POINT('Ctrl Pts',(2.31280267311102,9.80808834187509,0.921565983374903));
#93307=CARTESIAN_POINT('Ctrl Pts',(2.16857161230189,9.84098284917659,0.923902647974138));
#93308=CARTESIAN_POINT('Ctrl Pts',(2.02369901330553,9.87068479405285,0.926239312573372));
#93309=CARTESIAN_POINT('Ctrl Pts',(1.78194750865926,9.92024896225652,0.930138546704824));
#93310=CARTESIAN_POINT('Ctrl Pts',(1.53833954659131,9.96093457202526,0.934037780836275));
#93311=CARTESIAN_POINT('Ctrl Pts',(1.29354184001541,9.9926235548093,0.937937014967726));
#93312=CARTESIAN_POINT('Ctrl Pts',(1.04878424115534,10.0243073456627,0.941835610247708));
#93313=CARTESIAN_POINT('Ctrl Pts',(0.802837563134465,10.0469974163812,0.94573420552769));
#93314=CARTESIAN_POINT('Ctrl Pts',(0.556375673130158,10.0606273219094,0.949632800807672));
#93315=CARTESIAN_POINT('Ctrl Pts',(0.309938913293379,10.0742558376819,0.953530998572434));
#93316=CARTESIAN_POINT('Ctrl Pts',(0.0629873244840109,10.0788260175434,
0.957429196337196));
#93317=CARTESIAN_POINT('Ctrl Pts',(-0.18380210348543,10.0743234406462,0.961327394101958));
#93318=CARTESIAN_POINT('Ctrl Pts',(-0.430609909472234,10.0698205284493,
0.965225882159325));
#93319=CARTESIAN_POINT('Ctrl Pts',(-0.677255251833692,10.0562435117472,
0.969124370216694));
#93320=CARTESIAN_POINT('Ctrl Pts',(-0.923061836352939,10.0336300931552,
0.973022858274062));
#93321=CARTESIAN_POINT('Ctrl Pts',(-1.16886570418859,10.0110169244893,0.976921303244876));
#93322=CARTESIAN_POINT('Ctrl Pts',(-1.41383055543933,9.97936758131172,0.980819748215689));
#93323=CARTESIAN_POINT('Ctrl Pts',(-1.65728513653646,9.93877165328872,0.984718193186504));
#93324=CARTESIAN_POINT('Ctrl Pts',(-1.90078845796559,9.89816759784005,0.988617418637608));
#93325=CARTESIAN_POINT('Ctrl Pts',(-2.14278063006369,9.84861342389478,0.992516644088713));
#93326=CARTESIAN_POINT('Ctrl Pts',(-2.38259915674125,9.79025011214197,0.996415869539818));
#93327=CARTESIAN_POINT('Ctrl Pts',(-2.52631491628535,9.75527480062511,0.99875255367804));
#93328=CARTESIAN_POINT('Ctrl Pts',(-2.66925026464293,9.71713690675989,1.00108923781626));
#93329=CARTESIAN_POINT('Ctrl Pts',(-2.81126481973547,9.67587547012247,1.00342592195448));
#93330=CARTESIAN_POINT('Ctrl Pts',(-3.0482449078802,9.60702239457016,1.00732515335849));
#93331=CARTESIAN_POINT('Ctrl Pts',(-3.28272829929941,9.52944914124046,1.01122438476249));
#93332=CARTESIAN_POINT('Ctrl Pts',(-3.51407012138599,9.44336206983415,1.01512361616649));
#93333=CARTESIAN_POINT('Ctrl Pts',(-3.74537403774056,9.35728910393383,1.01902220867512));
#93334=CARTESIAN_POINT('Ctrl Pts',(-3.97353715134841,9.26270520197138,1.02292080118374));
#93335=CARTESIAN_POINT('Ctrl Pts',(-4.19793232657444,9.1598657294472,1.02681939369237));
#93336=CARTESIAN_POINT('Ctrl Pts',(-4.42230461957367,9.05703674376228,1.03071758865021));
#93337=CARTESIAN_POINT('Ctrl Pts',(-4.64290948820314,8.94595398455712,1.03461578360805));
#93338=CARTESIAN_POINT('Ctrl Pts',(-4.85914128733917,8.82692029813773,1.03851397856589));
#93339=CARTESIAN_POINT('Ctrl Pts',(-5.07538918704402,8.70787774849809,1.04241246378241));
#93340=CARTESIAN_POINT('Ctrl Pts',(-5.28726312115754,8.58088322060709,1.04631094899893));
#93341=CARTESIAN_POINT('Ctrl Pts',(-5.49418235928347,8.4462853493674,1.05020943421545));
#93342=CARTESIAN_POINT('Ctrl Pts',(-5.70109930973822,8.31168896622361,1.05410787633084));
#93343=CARTESIAN_POINT('Ctrl Pts',(-5.90306144133676,8.16948956156915,1.05800631844623));
#93344=CARTESIAN_POINT('Ctrl Pts',(-6.09951667220483,8.02007932413984,1.06190476056162));
#93345=CARTESIAN_POINT('Ctrl Pts',(-6.29601123380888,7.87063917447772,1.06580398315304));
#93346=CARTESIAN_POINT('Ctrl Pts',(-6.48699646955251,7.71398547575149,1.06970320574446));
#93347=CARTESIAN_POINT('Ctrl Pts',(-6.67195200307348,7.55055179895376,1.07360242833587));
#93348=CARTESIAN_POINT('Ctrl Pts',(-6.78279096391377,7.4526103177895,1.07593912933578));
#93349=CARTESIAN_POINT('Ctrl Pts',(-6.89146511561747,7.35223472945497,1.0782758303357));
#93350=CARTESIAN_POINT('Ctrl Pts',(-6.99786846164796,7.24952501847347,1.08061253133561));
#93351=CARTESIAN_POINT('Ctrl Pts',(-7.17542289291094,7.07813412712613,1.08451176601712));
#93352=CARTESIAN_POINT('Ctrl Pts',(-7.34670327209188,6.90019254495825,1.08841100069863));
#93353=CARTESIAN_POINT('Ctrl Pts',(-7.51123529203221,6.71618346888542,1.09231023538014));
#93354=CARTESIAN_POINT('Ctrl Pts',(-7.67574035495956,6.53220454095674,1.09620883120898));
#93355=CARTESIAN_POINT('Ctrl Pts',(-7.83349908025185,6.34216031129303,1.10010742703783));
#93356=CARTESIAN_POINT('Ctrl Pts',(-7.98407569837239,6.14656906270966,1.10400602286667));
#93357=CARTESIAN_POINT('Ctrl Pts',(-8.13463696303662,5.95099775747292,1.10790422117748));
#93358=CARTESIAN_POINT('Ctrl Pts',(-8.27801741291023,5.74988078341287,1.1118024194883));
#93359=CARTESIAN_POINT('Ctrl Pts',(-8.41382242583546,5.54376841025202,1.11570061779911));
#93360=CARTESIAN_POINT('Ctrl Pts',(-8.54963755165739,5.33764068866558,1.11959910639432));
#93361=CARTESIAN_POINT('Ctrl Pts',(-8.67787595768428,5.12651705582506,1.12349759498954));
#93362=CARTESIAN_POINT('Ctrl Pts',(-8.79818640959344,4.91097667496449,1.12739608358475));
#93363=CARTESIAN_POINT('Ctrl Pts',(-8.91849553164639,4.69543867658783,1.13129452908787));
#93364=CARTESIAN_POINT('Ctrl Pts',(-9.03087674088284,4.47548427217523,1.13519297459099));
#93365=CARTESIAN_POINT('Ctrl Pts',(-9.13502445222196,4.25171780076087,1.13909142009411));
#93366=CARTESIAN_POINT('Ctrl Pts',(-9.23919301391776,4.02790653133145,1.14299064606545));
#93367=CARTESIAN_POINT('Ctrl Pts',(-9.33512466596635,3.80028192242132,1.14688987203679));
#93368=CARTESIAN_POINT('Ctrl Pts',(-9.42256116463429,3.56947014257379,1.15078909800813));
#93369=CARTESIAN_POINT('Ctrl Pts',(-9.47495905030496,3.43115205532025,1.153125778911));
#93370=CARTESIAN_POINT('Ctrl Pts',(-9.52430706016383,3.29168977936706,1.15546245981386));
#93371=CARTESIAN_POINT('Ctrl Pts',(-9.57055803352992,3.15122118024678,1.15779914071672));
#93372=CARTESIAN_POINT('Ctrl Pts',(-9.64777480921259,2.91670649829887,1.16170026867116));
#93373=CARTESIAN_POINT('Ctrl Pts',(-9.71637906497317,2.67931785308615,1.16560139662559));
#93374=CARTESIAN_POINT('Ctrl Pts',(-9.77617606632402,2.43970439197731,1.16950252458003));
#93375=CARTESIAN_POINT('Ctrl Pts',(-9.83596427335629,2.20012617071438,1.1734030787973));
#93376=CARTESIAN_POINT('Ctrl Pts',(-9.88694774353637,1.95832405617931,1.17730363301457));
#93377=CARTESIAN_POINT('Ctrl Pts',(-9.92898217526058,1.71496033871275,1.18120418723184));
#93378=CARTESIAN_POINT('Ctrl Pts',(-9.97101121735301,1.4716278252085,1.18510424132219));
#93379=CARTESIAN_POINT('Ctrl Pts',(-10.0040934654087,1.22673438257842,1.18900429541253));
#93380=CARTESIAN_POINT('Ctrl Pts',(-10.0281359350344,0.980951409841928,
1.19290434950288));
#93381=CARTESIAN_POINT('Ctrl Pts',(-10.0521781282351,0.735171262962186,
1.19680435875288));
#93382=CARTESIAN_POINT('Ctrl Pts',(-10.067180722547,0.488501882977814,1.20070436800288));
#93383=CARTESIAN_POINT('Ctrl Pts',(-10.0731025921405,0.241619883725561,
1.20460437725288));
#93384=CARTESIAN_POINT('Ctrl Pts',(-10.0750355819202,0.161033782700128,
1.20587740056107));
#93385=CARTESIAN_POINT('Ctrl Pts',(-10.0760014602083,0.0804250515856432,
1.20715042386926));
#93386=CARTESIAN_POINT('Ctrl Pts',(-10.075999998343,-0.000182733646683074,
1.20842344717745));
#93387=CARTESIAN_POINT('Origin',(-12.,0.,2.));
#93388=CARTESIAN_POINT('',(-13.,1.22464679914735E-16,4.));
#93389=CARTESIAN_POINT('Origin',(-12.,0.,4.));
#93390=CARTESIAN_POINT('',(-13.,1.22464679914735E-16,2.77555756156289E-16));
#93391=CARTESIAN_POINT('',(-13.,1.22464679914735E-16,2.));
#93392=CARTESIAN_POINT('Origin',(-12.,0.,0.));
#93393=CARTESIAN_POINT('Origin',(12.,0.,2.));
#93394=CARTESIAN_POINT('',(11.,1.22464679914735E-16,4.));
#93395=CARTESIAN_POINT('Origin',(12.,0.,4.));
#93396=CARTESIAN_POINT('',(11.,1.22464679914735E-16,2.77555756156289E-16));
#93397=CARTESIAN_POINT('',(11.,1.22464679914735E-16,2.));
#93398=CARTESIAN_POINT('Origin',(12.,0.,0.));
#93399=CARTESIAN_POINT('Ctrl Pts',(7.17621738932614,-6.25041224556232,0.000500910460653174));
#93400=CARTESIAN_POINT('Ctrl Pts',(8.18687236526029,-5.09006444337945,0.0262352698176417));
#93401=CARTESIAN_POINT('Ctrl Pts',(9.63395471253335,-2.27150058536375,0.0776984989683351));
#93402=CARTESIAN_POINT('Ctrl Pts',(9.58138228729352,2.48258398187168,0.154890597912733));
#93403=CARTESIAN_POINT('Ctrl Pts',(7.31935428374419,6.66274001420286,0.232077207293848));
#93404=CARTESIAN_POINT('Ctrl Pts',(3.36913192154157,9.30677822701765,0.309263816674962));
#93405=CARTESIAN_POINT('Ctrl Pts',(-1.35804311095471,9.80414545245253,0.386450426056077));
#93406=CARTESIAN_POINT('Ctrl Pts',(-5.77204792492632,8.04051749446169,0.463637035437191));
#93407=CARTESIAN_POINT('Ctrl Pts',(-8.85483151763869,4.42244483853405,0.540823644818305));
#93408=CARTESIAN_POINT('Ctrl Pts',(-9.89543967406733,-0.215540505644021,
0.61801025419942));
#93409=CARTESIAN_POINT('Ctrl Pts',(-8.65386430243906,-4.80383258549442,
0.695196863580534));
#93410=CARTESIAN_POINT('Ctrl Pts',(-5.41645587973474,-8.28421130130496,
0.772383472961649));
#93411=CARTESIAN_POINT('Ctrl Pts',(-0.929852480502083,-9.85401182891119,
0.849570082342763));
#93412=CARTESIAN_POINT('Ctrl Pts',(3.77120163523642,-9.15118560282794,0.926756691723877));
#93413=CARTESIAN_POINT('Ctrl Pts',(7.60250616986962,-6.33782826253284,1.00394330110499));
#93414=CARTESIAN_POINT('Ctrl Pts',(9.68044931280096,-2.06278099798744,1.0811299104861));
#93415=CARTESIAN_POINT('Ctrl Pts',(9.52579656035691,2.68800387653829,1.15831651986722));
#93416=CARTESIAN_POINT('Ctrl Pts',(7.17421526680798,6.81885624067874,1.23550312924833));
#93417=CARTESIAN_POINT('Ctrl Pts',(3.16804921250801,9.37707998257651,1.31268973862945));
#93418=CARTESIAN_POINT('Ctrl Pts',(-1.5687620600508,9.77267366930781,1.38987634801056));
#93419=CARTESIAN_POINT('Ctrl Pts',(-5.9437707149038,7.91440172128742,1.46706295739167));
#93420=CARTESIAN_POINT('Ctrl Pts',(-8.94797124967819,4.23083626353518,1.54424956677279));
#93421=CARTESIAN_POINT('Ctrl Pts',(-9.88850677017832,-0.42848432033699,
1.6214361761539));
#93422=CARTESIAN_POINT('Ctrl Pts',(-8.54846215945662,-4.98898383099503,
1.69862278553501));
#93423=CARTESIAN_POINT('Ctrl Pts',(-5.23689106701696,-8.39887712217299,
1.77580939491613));
#93424=CARTESIAN_POINT('Ctrl Pts',(-0.717539063250466,-9.87174263493707,
1.85299600429724));
#93425=CARTESIAN_POINT('Ctrl Pts',(3.96729852598773,-9.06789431817403,1.93018261367836));
#93426=CARTESIAN_POINT('Ctrl Pts',(7.73716053739322,-6.17272320596467,2.00736922305947));
#93427=CARTESIAN_POINT('Ctrl Pts',(9.7226060531113,-1.85394080142852,2.08455583244059));
#93428=CARTESIAN_POINT('Ctrl Pts',(9.46573301557702,2.89241481066607,2.1617424418217));
#93429=CARTESIAN_POINT('Ctrl Pts',(7.02578389278733,6.9716946039717,2.23892905120282));
#93430=CARTESIAN_POINT('Ctrl Pts',(2.96548262493255,9.4430968310228,2.31611566058393));
#93431=CARTESIAN_POINT('Ctrl Pts',(-1.77874604604193,9.7366435419793,2.39330226996505));
#93432=CARTESIAN_POINT('Ctrl Pts',(-6.11274362884173,7.78463424226082,2.47048887934616));
#93433=CARTESIAN_POINT('Ctrl Pts',(-9.03696297170373,4.03725961627666,2.54767548872727));
#93434=CARTESIAN_POINT('Ctrl Pts',(-9.87699319615832,-0.641225670598249,
2.62486209810839));
#93435=CARTESIAN_POINT('Ctrl Pts',(-8.4390986575348,-5.17182548091403,2.7020487074895));
#93436=CARTESIAN_POINT('Ctrl Pts',(-5.05490007275752,-8.50965041751702,
2.77923531687063));
#93437=CARTESIAN_POINT('Ctrl Pts',(-0.504893047272655,-9.88489999585637,
2.85642192625173));
#93438=CARTESIAN_POINT('Ctrl Pts',(4.16155714909012,-8.98040127960293,2.93360853563285));
#93439=CARTESIAN_POINT('Ctrl Pts',(7.86823001667005,-6.00475821472291,3.01079514501396));
#93440=CARTESIAN_POINT('Ctrl Pts',(9.76025792883615,-1.6442415540714,3.08798175439507));
#93441=CARTESIAN_POINT('Ctrl Pts',(9.40128363486594,3.09548557845033,3.16516836377619));
#93442=CARTESIAN_POINT('Ctrl Pts',(6.87409722408249,7.12130266855917,3.2423549731573));
#93443=CARTESIAN_POINT('Ctrl Pts',(2.76154197480476,9.50473845351135,3.31954158253842));
#93444=CARTESIAN_POINT('Ctrl Pts',(-1.98790578544033,9.69610180945044,3.39672819191953));
#93445=CARTESIAN_POINT('Ctrl Pts',(-6.27888444807983,7.6512603437263,3.47391480130065));
#93446=CARTESIAN_POINT('Ctrl Pts',(-9.12176718588067,3.84181136814036,3.55110141068176));
#93447=CARTESIAN_POINT('Ctrl Pts',(-9.86090390749274,-0.853667969225371,
3.62828802006288));
#93448=CARTESIAN_POINT('Ctrl Pts',(-8.32582367444923,-5.35227467481443,
3.70547462944399));
#93449=CARTESIAN_POINT('Ctrl Pts',(-4.870569570912,-8.61647326987962,3.78266123882511));
#93450=CARTESIAN_POINT('Ctrl Pts',(-0.292007921251256,-9.89349231567484,
3.85984784820622));
#93451=CARTESIAN_POINT('Ctrl Pts',(4.35387734572572,-8.88871763543166,3.93703445758733));
#93452=CARTESIAN_POINT('Ctrl Pts',(7.99567403095283,-5.83406956269694,4.01422106696845));
#93453=CARTESIAN_POINT('Ctrl Pts',(9.79334762174143,-1.43366453103774,4.09140767634956));
#93454=CARTESIAN_POINT('Ctrl Pts',(9.33255727203353,3.29689012957999,4.16859428573068));
#93455=CARTESIAN_POINT('Ctrl Pts',(6.71906686705208,7.26810366491508,4.24578089511179));
#93456=CARTESIAN_POINT('Ctrl Pts',(3.944124220863,8.79638862890064,4.2972386346992));
#93457=CARTESIAN_POINT('Ctrl Pts',(2.45787321508261,9.19372658581085,4.3229675044929));
#93458=CARTESIAN_POINT('Ctrl Pts',(7.31697141119783,-6.37300756482166,-0.107266287678314));
#93459=CARTESIAN_POINT('Ctrl Pts',(8.3474493307344,-5.18990075032541,-0.0815319283213253));
#93460=CARTESIAN_POINT('Ctrl Pts',(9.82291468946153,-2.31605370098554,-0.0300686991706319));
#93461=CARTESIAN_POINT('Ctrl Pts',(9.76931111091479,2.53127727823173,0.0471233997737662));
#93462=CARTESIAN_POINT('Ctrl Pts',(7.46291578655946,6.79342271273417,0.124310009154881));
#93463=CARTESIAN_POINT('Ctrl Pts',(3.43521393138684,9.48932097831013,0.201496618535995));
#93464=CARTESIAN_POINT('Ctrl Pts',(-1.38467971062437,9.99644354329634,0.278683227917109));
#93465=CARTESIAN_POINT('Ctrl Pts',(-5.88526062679874,8.1982238617407,0.355869837298224));
#93466=CARTESIAN_POINT('Ctrl Pts',(-9.02850980544496,4.50918648301867,0.433056446679338));
#93467=CARTESIAN_POINT('Ctrl Pts',(-10.089528405881,-0.219768107930814,
0.510243056060454));
#93468=CARTESIAN_POINT('Ctrl Pts',(-8.82360082785589,-4.89805475298508,
0.587429665441566));
#93469=CARTESIAN_POINT('Ctrl Pts',(-5.52269401439564,-8.44669746852,0.664616274822683));
#93470=CARTESIAN_POINT('Ctrl Pts',(-0.948090567404625,-10.0472879967365,
0.741802884203794));
#93471=CARTESIAN_POINT('Ctrl Pts',(3.84516982330136,-9.33067656702422,0.818989493584912));
#93472=CARTESIAN_POINT('Ctrl Pts',(7.75162140170541,-6.4621381558215,0.896176102966023));
#93473=CARTESIAN_POINT('Ctrl Pts',(9.8703212328362,-2.10324029652249,0.973362712347141));
#93474=CARTESIAN_POINT('Ctrl Pts',(9.71263512790029,2.74072626995299,1.05054932172825));
#93475=CARTESIAN_POINT('Ctrl Pts',(7.31493001913396,6.95260099621914,1.12773593110937));
#93476=CARTESIAN_POINT('Ctrl Pts',(3.2301871946727,9.56100162950478,1.20492254049048));
#93477=CARTESIAN_POINT('Ctrl Pts',(-1.59953169220272,9.96435447393901,1.2821091498716));
#93478=CARTESIAN_POINT('Ctrl Pts',(-6.06035158025637,8.06963445916912,1.35929575925271));
#93479=CARTESIAN_POINT('Ctrl Pts',(-9.12347637621708,4.31381970560019,1.43648236863382));
#93480=CARTESIAN_POINT('Ctrl Pts',(-10.0824595203107,-0.436888593524985,
1.51366897801494));
#93481=CARTESIAN_POINT('Ctrl Pts',(-8.71613133173546,-5.08683754711988,
1.59085558739605));
#93482=CARTESIAN_POINT('Ctrl Pts',(-5.33960722509808,-8.56361233990904,
1.66804219677717));
#93483=CARTESIAN_POINT('Ctrl Pts',(-0.73161284384033,-10.0653665740357,
1.74522880615828));
#93484=CARTESIAN_POINT('Ctrl Pts',(4.04511295010607,-9.24575161066474,1.82241541553939));
#93485=CARTESIAN_POINT('Ctrl Pts',(7.88891687425179,-6.2937947357141,1.89960202492051));
#93486=CARTESIAN_POINT('Ctrl Pts',(9.91330483365338,-1.89030391725346,1.97678863430162));
#93487=CARTESIAN_POINT('Ctrl Pts',(9.65139349931427,2.94914651142642,2.05397524368274));
#93488=CARTESIAN_POINT('Ctrl Pts',(7.16358731847254,7.10843712465253,2.13116185306385));
#93489=CARTESIAN_POINT('Ctrl Pts',(3.02364747468623,9.62831332960143,2.20834846244497));
#93490=CARTESIAN_POINT('Ctrl Pts',(-1.81363429514113,9.92761765322946,2.28553507182608));
#93491=CARTESIAN_POINT('Ctrl Pts',(-6.23263872172306,7.93732172634232,2.36272168120719));
#93492=CARTESIAN_POINT('Ctrl Pts',(-9.21421357808373,4.1164462542367,2.43990829058831));
#93493=CARTESIAN_POINT('Ctrl Pts',(-10.0707201195409,-0.653802643558734,
2.51709489996942));
#93494=CARTESIAN_POINT('Ctrl Pts',(-8.60462277875034,-5.2732654453638,2.59428150935053));
#93495=CARTESIAN_POINT('Ctrl Pts',(-5.15404666723755,-8.67655833794445,
2.67146811873166));
#93496=CARTESIAN_POINT('Ctrl Pts',(-0.514795997972617,-10.078782002871,
2.74865472811276));
#93497=CARTESIAN_POINT('Ctrl Pts',(4.24318175355855,-9.15654248736592,2.82584133749388));
#93498=CARTESIAN_POINT('Ctrl Pts',(8.0225571447062,-6.12253528629633,2.90302794687499));
#93499=CARTESIAN_POINT('Ctrl Pts',(9.95169521166317,-1.67649163780051,2.98021455625611));
#93500=CARTESIAN_POINT('Ctrl Pts',(9.58568001119813,3.15620030059083,3.05740116563722));
#93501=CARTESIAN_POINT('Ctrl Pts',(7.00892547391585,7.26097959543934,3.13458777501834));
#93502=CARTESIAN_POINT('Ctrl Pts',(2.81570674134309,9.691163988245,3.21177438439945));
#93503=CARTESIAN_POINT('Ctrl Pts',(-2.02689648474925,9.88628073688752,3.28896099378057));
#93504=CARTESIAN_POINT('Ctrl Pts',(-6.40203821990527,7.80133183784919,3.36614760316168));
#93505=CARTESIAN_POINT('Ctrl Pts',(-9.30068113850137,3.91716449249559,3.4433342125428));
#93506=CARTESIAN_POINT('Ctrl Pts',(-10.0543152562534,-0.870411776372325,
3.52052082192391));
#93507=CARTESIAN_POINT('Ctrl Pts',(-8.48912602497671,-5.45725396205879,
3.59770743130503));
#93508=CARTESIAN_POINT('Ctrl Pts',(-4.9661007147889,-8.78547640917823,3.67489404068614));
#93509=CARTESIAN_POINT('Ctrl Pts',(-0.297735352167109,-10.0875428520841,
3.75208065006725));
#93510=CARTESIAN_POINT('Ctrl Pts',(4.4392741103302,-9.06306056410737,3.82926725944837));
#93511=CARTESIAN_POINT('Ctrl Pts',(8.15250084045075,-5.94849875432791,3.90645386882949));
#93512=CARTESIAN_POINT('Ctrl Pts',(9.98543392439411,-1.46178436601633,3.98364047821059));
#93513=CARTESIAN_POINT('Ctrl Pts',(9.51560565241569,3.3615551919982,4.06082708759171));
#93514=CARTESIAN_POINT('Ctrl Pts',(6.85085435807332,7.41065994027801,4.13801369697282));
#93515=CARTESIAN_POINT('Ctrl Pts',(4.02148410514878,8.96892062037927,4.18947143656024));
#93516=CARTESIAN_POINT('Ctrl Pts',(2.50608183551656,9.37405194703336,4.21520030635394));
#93517=CARTESIAN_POINT('Ctrl Pts',(7.4577254330695,-6.49560288408101,-0.215033485817281));
#93518=CARTESIAN_POINT('Ctrl Pts',(8.50802629620849,-5.28973705727136,-0.189299126460293));
#93519=CARTESIAN_POINT('Ctrl Pts',(10.0118746663897,-2.36060681660734,-0.137835897309599));
#93520=CARTESIAN_POINT('Ctrl Pts',(9.95723993453606,2.57997057459178,-0.0606437983652013));
#93521=CARTESIAN_POINT('Ctrl Pts',(7.60647728937472,6.92410541126547,0.0165428110159138));
#93522=CARTESIAN_POINT('Ctrl Pts',(3.50129594123211,9.67186372960258,0.0937294203970275));
#93523=CARTESIAN_POINT('Ctrl Pts',(-1.41131631029405,10.1887416341402,0.170916029778142));
#93524=CARTESIAN_POINT('Ctrl Pts',(-5.99847332867116,8.3559302290197,0.248102639159256));
#93525=CARTESIAN_POINT('Ctrl Pts',(-9.20218809325122,4.5959281275033,0.325289248540371));
#93526=CARTESIAN_POINT('Ctrl Pts',(-10.2836171376947,-0.223995710217611,
0.402475857921486));
#93527=CARTESIAN_POINT('Ctrl Pts',(-8.99333735327271,-4.99227692047576,
0.479662467302599));
#93528=CARTESIAN_POINT('Ctrl Pts',(-5.62893214905654,-8.60918363573503,
0.556849076683716));
#93529=CARTESIAN_POINT('Ctrl Pts',(-0.966328654307157,-10.2405641645618,
0.634035686064827));
#93530=CARTESIAN_POINT('Ctrl Pts',(3.9191380113663,-9.51016753122048,0.711222295445945));
#93531=CARTESIAN_POINT('Ctrl Pts',(7.9007366335412,-6.58644804911019,0.788408904827056));
#93532=CARTESIAN_POINT('Ctrl Pts',(10.0601931528714,-2.14369959505755,0.865595514208172));
#93533=CARTESIAN_POINT('Ctrl Pts',(9.89947369544367,2.79344866336769,0.942782123589285));
#93534=CARTESIAN_POINT('Ctrl Pts',(7.45564477145993,7.08634575175956,1.0199687329704));
#93535=CARTESIAN_POINT('Ctrl Pts',(3.29232517683739,9.74492327643303,1.09715534235151));
#93536=CARTESIAN_POINT('Ctrl Pts',(-1.63030132435465,10.1560352785702,1.17434195173263));
#93537=CARTESIAN_POINT('Ctrl Pts',(-6.17693244560895,8.22486719705081,1.25152856111374));
#93538=CARTESIAN_POINT('Ctrl Pts',(-9.29898150275598,4.39680314766522,1.32871517049486));
#93539=CARTESIAN_POINT('Ctrl Pts',(-10.2764122704431,-0.445292866712986,
1.40590177987597));
#93540=CARTESIAN_POINT('Ctrl Pts',(-8.8838005040143,-5.18469126324474,1.48308838925709));
#93541=CARTESIAN_POINT('Ctrl Pts',(-5.4423233831792,-8.72834755764508,1.5602749986382));
#93542=CARTESIAN_POINT('Ctrl Pts',(-0.745686624430195,-10.2589905131343,
1.63746160801931));
#93543=CARTESIAN_POINT('Ctrl Pts',(4.12292737422438,-9.42360890315545,1.71464821740043));
#93544=CARTESIAN_POINT('Ctrl Pts',(8.04067321111036,-6.41486626546352,1.79183482678154));
#93545=CARTESIAN_POINT('Ctrl Pts',(10.1040036141955,-1.92666703307842,1.86902143616266));
#93546=CARTESIAN_POINT('Ctrl Pts',(9.83705398305152,3.00587821218677,1.94620804554377));
#93547=CARTESIAN_POINT('Ctrl Pts',(7.30139074415778,7.24517964533336,2.02339465492489));
#93548=CARTESIAN_POINT('Ctrl Pts',(3.0818123244399,9.81352982818008,2.100581264306));
#93549=CARTESIAN_POINT('Ctrl Pts',(-1.84852254424032,10.1185917644796,2.17776787368711));
#93550=CARTESIAN_POINT('Ctrl Pts',(-6.35253381460441,8.09000921042384,2.25495448306823));
#93551=CARTESIAN_POINT('Ctrl Pts',(-9.39146418446372,4.19563289219672,2.33214109244934));
#93552=CARTESIAN_POINT('Ctrl Pts',(-10.2644470429234,-0.666379616519211,
2.40932770183046));
#93553=CARTESIAN_POINT('Ctrl Pts',(-8.77014689996588,-5.37470540981357,
2.48651431121157));
#93554=CARTESIAN_POINT('Ctrl Pts',(-5.25319326171758,-8.84346625837187,
2.56370092059269));
#93555=CARTESIAN_POINT('Ctrl Pts',(-0.524698948672571,-10.2726640098856,
2.6408875299738));
#93556=CARTESIAN_POINT('Ctrl Pts',(4.32480635802698,-9.33268369512891,2.71807413935492));
#93557=CARTESIAN_POINT('Ctrl Pts',(8.17688427274236,-6.24031235786978,2.79526074873603));
#93558=CARTESIAN_POINT('Ctrl Pts',(10.1431324944901,-1.70874172152963,2.87244735811714));
#93559=CARTESIAN_POINT('Ctrl Pts',(9.77007638753031,3.21691502273131,2.94963396749826));
#93560=CARTESIAN_POINT('Ctrl Pts',(7.14375372374919,7.40065652231953,3.02682057687937));
#93561=CARTESIAN_POINT('Ctrl Pts',(2.86987150788144,9.87758952297865,3.10400718626049));
#93562=CARTESIAN_POINT('Ctrl Pts',(-2.06588718405818,10.0764596643246,3.1811937956416));
#93563=CARTESIAN_POINT('Ctrl Pts',(-6.52519199173069,7.95140333197205,3.25838040502272));
#93564=CARTESIAN_POINT('Ctrl Pts',(-9.47959509112208,3.99251761685082,3.33556701440383));
#93565=CARTESIAN_POINT('Ctrl Pts',(-10.2477266050142,-0.88715558351928,
3.41275362378494));
#93566=CARTESIAN_POINT('Ctrl Pts',(-8.65242837550419,-5.56223324930316,
3.48994023316606));
#93567=CARTESIAN_POINT('Ctrl Pts',(-5.06163185866582,-8.95447954847683,
3.56712684254717));
#93568=CARTESIAN_POINT('Ctrl Pts',(-0.303462783082962,-10.2815933884932,
3.64431345192829));
#93569=CARTESIAN_POINT('Ctrl Pts',(4.52467087493469,-9.23740349278308,3.7215000613094));
#93570=CARTESIAN_POINT('Ctrl Pts',(8.30932764994867,-6.06292794595889,3.79868667069052));
#93571=CARTESIAN_POINT('Ctrl Pts',(10.1775202270467,-1.48990420099491,3.87587328007163));
#93572=CARTESIAN_POINT('Ctrl Pts',(9.69865403279785,3.42622025441641,3.95305988945275));
#93573=CARTESIAN_POINT('Ctrl Pts',(6.98264184909456,7.55321621564095,4.03024649883386));
#93574=CARTESIAN_POINT('Ctrl Pts',(4.09884398943458,9.14145261185791,4.08170423842127));
#93575=CARTESIAN_POINT('Ctrl Pts',(2.55429045595051,9.55437730825585,4.10743310821497));
#93576=CARTESIAN_POINT('Ctrl Pts',(7.59847945494118,-6.61819820334034,-0.322800683956248));
#93577=CARTESIAN_POINT('Ctrl Pts',(8.6686032616826,-5.38957336421732,-0.297066324599259));
#93578=CARTESIAN_POINT('Ctrl Pts',(10.2008346433178,-2.40515993222915,-0.245603095448566));
#93579=CARTESIAN_POINT('Ctrl Pts',(10.1451687581573,2.62866387095184,-0.168410996504169));
#93580=CARTESIAN_POINT('Ctrl Pts',(7.75003879218998,7.05478810979676,-0.0912243871230533));
#93581=CARTESIAN_POINT('Ctrl Pts',(3.56737795107737,9.85440648089508,-0.0140377777419394));
#93582=CARTESIAN_POINT('Ctrl Pts',(-1.43795290996372,10.381039724984,0.0631488316391753));
#93583=CARTESIAN_POINT('Ctrl Pts',(-6.11168603054357,8.51363659629871,0.140335441020289));
#93584=CARTESIAN_POINT('Ctrl Pts',(-9.37586638105749,4.68266977198792,0.217522050401404));
#93585=CARTESIAN_POINT('Ctrl Pts',(-10.4777058695083,-0.228223312504405,
0.294708659782519));
#93586=CARTESIAN_POINT('Ctrl Pts',(-9.16307387868954,-5.08649908796642,
0.371895269163633));
#93587=CARTESIAN_POINT('Ctrl Pts',(-5.73517028371745,-8.77166980295006,
0.449081878544748));
#93588=CARTESIAN_POINT('Ctrl Pts',(-0.984566741209693,-10.4338403323871,
0.526268487925861));
#93589=CARTESIAN_POINT('Ctrl Pts',(3.99310619943123,-9.68965849541676,0.603455097306976));
#93590=CARTESIAN_POINT('Ctrl Pts',(8.04985186537699,-6.71075794239885,0.68064170668809));
#93591=CARTESIAN_POINT('Ctrl Pts',(10.2500650729067,-2.18415889359261,0.757828316069205));
#93592=CARTESIAN_POINT('Ctrl Pts',(10.086312262987,2.84617105678237,0.835014925450318));
#93593=CARTESIAN_POINT('Ctrl Pts',(7.59635952378591,7.22009050729999,0.912201534831435));
#93594=CARTESIAN_POINT('Ctrl Pts',(3.35446315900208,9.92884492336128,0.989388144212546));
#93595=CARTESIAN_POINT('Ctrl Pts',(-1.66107095650658,10.3477160832014,1.06657475359366));
#93596=CARTESIAN_POINT('Ctrl Pts',(-6.29351331096151,8.38009993493251,1.14376136297478));
#93597=CARTESIAN_POINT('Ctrl Pts',(-9.47448662929488,4.47978658973023,1.22094797235589));
#93598=CARTESIAN_POINT('Ctrl Pts',(-10.4703650205756,-0.453697139900987,
1.29813458173701));
#93599=CARTESIAN_POINT('Ctrl Pts',(-9.05146967629314,-5.28254497936959,
1.37532119111812));
#93600=CARTESIAN_POINT('Ctrl Pts',(-5.54503954126032,-8.89308277538113,
1.45250780049923));
#93601=CARTESIAN_POINT('Ctrl Pts',(-0.759760405020054,-10.452614452233,
1.52969440988035));
#93602=CARTESIAN_POINT('Ctrl Pts',(4.20074179834271,-9.60146619564616,1.60688101926146));
#93603=CARTESIAN_POINT('Ctrl Pts',(8.19242954796893,-6.53593779521296,1.68406762864258));
#93604=CARTESIAN_POINT('Ctrl Pts',(10.2947023947376,-1.96303014890336,1.76125423802369));
#93605=CARTESIAN_POINT('Ctrl Pts',(10.0227144667888,3.06260991294711,1.83844084740481));
#93606=CARTESIAN_POINT('Ctrl Pts',(7.43919416984301,7.3819221660142,1.91562745678592));
#93607=CARTESIAN_POINT('Ctrl Pts',(3.13997717419355,9.99874632675871,1.99281406616704));
#93608=CARTESIAN_POINT('Ctrl Pts',(-1.8834107933395,10.3095658757298,2.07000067554815));
#93609=CARTESIAN_POINT('Ctrl Pts',(-6.47242890748576,8.24269669450534,2.14718728492927));
#93610=CARTESIAN_POINT('Ctrl Pts',(-9.5687147908437,4.27481953015676,2.22437389431038));
#93611=CARTESIAN_POINT('Ctrl Pts',(-10.458173966306,-0.678956589479688,
2.30156050369149));
#93612=CARTESIAN_POINT('Ctrl Pts',(-8.93567102118141,-5.47614537426334,
2.37874711307261));
#93613=CARTESIAN_POINT('Ctrl Pts',(-5.35233985619761,-9.01037417879928,
2.45593372245372));
#93614=CARTESIAN_POINT('Ctrl Pts',(-0.534601899372525,-10.4665460169004,
2.53312033183484));
#93615=CARTESIAN_POINT('Ctrl Pts',(4.40643096249542,-9.5088249028919,2.61030694121595));
#93616=CARTESIAN_POINT('Ctrl Pts',(8.33121140077849,-6.35808942944322,2.68749355059706));
#93617=CARTESIAN_POINT('Ctrl Pts',(10.3345697773172,-1.74099180525873,2.76468015997818));
#93618=CARTESIAN_POINT('Ctrl Pts',(9.9544727638625,3.27762974487179,2.84186676935929));
#93619=CARTESIAN_POINT('Ctrl Pts',(7.27858197358255,7.54033344919971,2.9190533787404));
#93620=CARTESIAN_POINT('Ctrl Pts',(2.92403627441977,10.0640150577123,2.99623998812152));
#93621=CARTESIAN_POINT('Ctrl Pts',(-2.10487788336711,10.2666385917617,3.07342659750264));
#93622=CARTESIAN_POINT('Ctrl Pts',(-6.64834576355613,8.10147482609493,3.15061320688375));
#93623=CARTESIAN_POINT('Ctrl Pts',(-9.65850904374278,4.06787074120605,3.22779981626486));
#93624=CARTESIAN_POINT('Ctrl Pts',(-10.4411379537749,-0.903899390666233,
3.30498642564598));
#93625=CARTESIAN_POINT('Ctrl Pts',(-8.81573072603167,-5.66721253654752,
3.38217303502709));
#93626=CARTESIAN_POINT('Ctrl Pts',(-5.15716300254271,-9.12348268777542,
3.45935964440821));
#93627=CARTESIAN_POINT('Ctrl Pts',(-0.309190213998818,-10.4756439249024,
3.53654625378932));
#93628=CARTESIAN_POINT('Ctrl Pts',(4.61006763953917,-9.41174642145879,3.61373286317044));
#93629=CARTESIAN_POINT('Ctrl Pts',(8.46615445944659,-6.17735713758986,3.69091947255155));
#93630=CARTESIAN_POINT('Ctrl Pts',(10.3696065296995,-1.5180240359735,3.76810608193267));
#93631=CARTESIAN_POINT('Ctrl Pts',(9.88170241318002,3.49088531683462,3.84529269131378));
#93632=CARTESIAN_POINT('Ctrl Pts',(7.1144293401158,7.69577249100388,3.9224793006949));
#93633=CARTESIAN_POINT('Ctrl Pts',(4.17620387372036,9.31398460333654,3.9739370402823));
#93634=CARTESIAN_POINT('Ctrl Pts',(2.60249907638446,9.73470266947836,3.99966591007601));
#93635=CARTESIAN_POINT('Ctrl Pts',(2.6023496244676,9.73414364143212,4.));
#93636=CARTESIAN_POINT('Ctrl Pts',(2.83853694256798,9.66402616844161,4.));
#93637=CARTESIAN_POINT('Ctrl Pts',(3.07166134324788,9.58522029115185,4.));
#93638=CARTESIAN_POINT('Ctrl Pts',(3.30132667682908,9.49806665648961,4.));
#93639=CARTESIAN_POINT('Ctrl Pts',(3.5400502322276,9.40747559858787,4.));
#93640=CARTESIAN_POINT('Ctrl Pts',(3.77503717013813,9.30786527649238,4.));
#93641=CARTESIAN_POINT('Ctrl Pts',(4.00582730120758,9.19956194039239,4.));
#93642=CARTESIAN_POINT('Ctrl Pts',(4.23171368243693,9.09355979656879,4.));
#93643=CARTESIAN_POINT('Ctrl Pts',(4.45358020203394,8.9792295867419,4.));
#93644=CARTESIAN_POINT('Ctrl Pts',(4.67097238674394,8.85682947856375,4.));
#93645=CARTESIAN_POINT('Ctrl Pts',(4.89544359643902,8.73044360877633,4.));
#93646=CARTESIAN_POINT('Ctrl Pts',(5.11514514178304,8.59545357942288,4.));
#93647=CARTESIAN_POINT('Ctrl Pts',(5.32954166532511,8.45209673940295,4.));
#93648=CARTESIAN_POINT('Ctrl Pts',(5.54393818886718,8.30873989938302,4.));
#93649=CARTESIAN_POINT('Ctrl Pts',(5.75303036100492,8.15701585598298,4.));
#93650=CARTESIAN_POINT('Ctrl Pts',(5.95623735557635,7.99712024365205,4.));
#93651=CARTESIAN_POINT('Ctrl Pts',(5.97890496335302,7.97928399233023,4.));
#93652=CARTESIAN_POINT('Ctrl Pts',(6.00149928764221,7.96134602092925,4.));
#93653=CARTESIAN_POINT('Ctrl Pts',(6.02401948143154,7.94330657213126,4.));
#93654=CARTESIAN_POINT('Ctrl Pts',(6.0505106021892,7.92208627442959,4.00000000000001));
#93655=CARTESIAN_POINT('Ctrl Pts',(6.07689301758066,7.9007304096383,4.00000000000001));
#93656=CARTESIAN_POINT('Ctrl Pts',(6.10315549849619,7.87924789105142,4.00000000000001));
#93657=CARTESIAN_POINT('Ctrl Pts',(6.29514744453683,7.72219987404892,4.00000000000001));
#93658=CARTESIAN_POINT('Ctrl Pts',(6.48089722280961,7.55825453484683,4.));
#93659=CARTESIAN_POINT('Ctrl Pts',(6.65998212635876,7.38768689939716,4.));
#93660=CARTESIAN_POINT('Ctrl Pts',(6.69015407484989,7.35894992710609,4.));
#93661=CARTESIAN_POINT('Ctrl Pts',(6.72013677327834,7.33002488212823,4.));
#93662=CARTESIAN_POINT('Ctrl Pts',(6.74992811418605,7.30091296200115,4.));
#93663=CARTESIAN_POINT('Ctrl Pts',(6.9262582868153,7.12860417209207,4.));
#93664=CARTESIAN_POINT('Ctrl Pts',(7.09588772648024,6.94975169953822,4.));
#93665=CARTESIAN_POINT('Ctrl Pts',(7.25857969279764,6.76483090696196,4.));
#93666=CARTESIAN_POINT('Ctrl Pts',(7.42201105991826,6.5790696882377,4.));
#93667=CARTESIAN_POINT('Ctrl Pts',(7.57844211565621,6.38718430988767,4.00000000000001));
#93668=CARTESIAN_POINT('Ctrl Pts',(7.72759196996615,6.18962354908701,4.00000000000001));
#93669=CARTESIAN_POINT('Ctrl Pts',(7.8762793761675,5.99267533732698,4.));
#93670=CARTESIAN_POINT('Ctrl Pts',(8.0177309789071,5.7900863001285,4.));
#93671=CARTESIAN_POINT('Ctrl Pts',(8.15162291233038,5.58227682514063,4.));
#93672=CARTESIAN_POINT('Ctrl Pts',(8.26759771712329,5.40227596415038,4.00000000000001));
#93673=CARTESIAN_POINT('Ctrl Pts',(8.37790014202984,5.21835776304691,4.));
#93674=CARTESIAN_POINT('Ctrl Pts',(8.48228911756457,5.03078568934111,4.));
#93675=CARTESIAN_POINT('Ctrl Pts',(8.50112007146166,4.99694915579681,4.));
#93676=CARTESIAN_POINT('Ctrl Pts',(8.51975857415101,4.96299335747099,4.));
#93677=CARTESIAN_POINT('Ctrl Pts',(8.53818915232497,4.92894630654343,4.));
#93678=CARTESIAN_POINT('Ctrl Pts',(8.65535538855079,4.71250356806194,4.));
#93679=CARTESIAN_POINT('Ctrl Pts',(8.76426876468842,4.49211446879426,4.));
#93680=CARTESIAN_POINT('Ctrl Pts',(8.86469547420092,4.2682386905176,4.));
#93681=CARTESIAN_POINT('Ctrl Pts',(8.96498207431523,4.04467525046966,4.));
#93682=CARTESIAN_POINT('Ctrl Pts',(9.0568059746215,3.8176342698159,4.));
#93683=CARTESIAN_POINT('Ctrl Pts',(9.13988914425725,3.58754843136135,4.));
#93684=CARTESIAN_POINT('Ctrl Pts',(9.1781696365212,3.48153659770576,4.));
#93685=CARTESIAN_POINT('Ctrl Pts',(9.21459390332125,3.37487807624388,4.));
#93686=CARTESIAN_POINT('Ctrl Pts',(9.24913123944987,3.26761391216937,3.99999999999999));
#93687=CARTESIAN_POINT('Ctrl Pts',(9.32430819331323,3.03413345253597,3.99999999999999));
#93688=CARTESIAN_POINT('Ctrl Pts',(9.39054833689072,2.797783920754,3.99999999999999));
#93689=CARTESIAN_POINT('Ctrl Pts',(9.44781367990102,2.55908882180367,3.99999999999999));
#93690=CARTESIAN_POINT('Ctrl Pts',(9.50492475352923,2.32103675306121,3.99999999999999));
#93691=CARTESIAN_POINT('Ctrl Pts',(9.55310933215745,2.08065107338521,3.99999999999999));
#93692=CARTESIAN_POINT('Ctrl Pts',(9.59227815520829,1.83844879803419,3.99999999999999));
#93693=CARTESIAN_POINT('Ctrl Pts',(9.6139614565568,1.7043690755744,3.99999999999999));
#93694=CARTESIAN_POINT('Ctrl Pts',(9.63288089979977,1.56973266133125,3.99999999999998));
#93695=CARTESIAN_POINT('Ctrl Pts',(9.64901448005129,1.43462810174663,3.99999999999999));
#93696=CARTESIAN_POINT('Ctrl Pts',(9.65375203401828,1.39495524970519,3.99999999999999));
#93697=CARTESIAN_POINT('Ctrl Pts',(9.6582496986183,1.35523779998252,3.99999999999999));
#93698=CARTESIAN_POINT('Ctrl Pts',(9.66250334791277,1.31551317054319,3.99999999999999));
#93699=CARTESIAN_POINT('Ctrl Pts',(9.68848620150609,1.07286053058192,3.99999999999999));
#93700=CARTESIAN_POINT('Ctrl Pts',(9.70540234538228,0.829675292048995,3.99999999999999));
#93701=CARTESIAN_POINT('Ctrl Pts',(9.71327562900262,0.586475884702219,3.99999999999999));
#93702=CARTESIAN_POINT('Ctrl Pts',(9.72116108183257,0.342900580244727,3.99999999999999));
#93703=CARTESIAN_POINT('Ctrl Pts',(9.71997572067835,0.099310397190577,3.99999999999998));
#93704=CARTESIAN_POINT('Ctrl Pts',(9.70969154440537,-0.143780047697638,
3.99999999999999));
#93705=CARTESIAN_POINT('Ctrl Pts',(9.69949615601932,-0.38477178420512,3.99999999999999));
#93706=CARTESIAN_POINT('Ctrl Pts',(9.68035832847905,-0.625273010146937,
3.99999999999998));
#93707=CARTESIAN_POINT('Ctrl Pts',(9.65220012606401,-0.864778721030272,
3.99999999999999));
#93708=CARTESIAN_POINT('Ctrl Pts',(9.63108912131042,-1.04434296048145,3.99999999999999));
#93709=CARTESIAN_POINT('Ctrl Pts',(9.60490679924936,-1.22334761187656,3.99999999999999));
#93710=CARTESIAN_POINT('Ctrl Pts',(9.57360159863658,-1.4015752955962,3.99999999999999));
#93711=CARTESIAN_POINT('Ctrl Pts',(9.54008127908224,-1.59241415926013,3.99999999999999));
#93712=CARTESIAN_POINT('Ctrl Pts',(9.50068747829056,-1.7823624612145,3.99999999999999));
#93713=CARTESIAN_POINT('Ctrl Pts',(9.4555050228853,-1.9711691265491,3.99999999999999));
#93714=CARTESIAN_POINT('Ctrl Pts',(9.43573769864551,-2.05377204263296,3.99999999999999));
#93715=CARTESIAN_POINT('Ctrl Pts',(9.41486214872224,-2.13615632006512,3.99999999999999));
#93716=CARTESIAN_POINT('Ctrl Pts',(9.39288438044855,-2.21830029733162,3.99999999999999));
#93717=CARTESIAN_POINT('Ctrl Pts',(9.38127565021983,-2.26168901906741,3.99999999999999));
#93718=CARTESIAN_POINT('Ctrl Pts',(9.36935939152565,-2.30501069026336,4.));
#93719=CARTESIAN_POINT('Ctrl Pts',(9.35713641742303,-2.34826206837094,4.));
#93720=CARTESIAN_POINT('Ctrl Pts',(9.34817713074373,-2.37996478593278,4.));
#93721=CARTESIAN_POINT('Ctrl Pts',(9.33905529757631,-2.41162171069674,4.));
#93722=CARTESIAN_POINT('Ctrl Pts',(9.32977347375216,-2.44322504264465,4.));
#93723=CARTESIAN_POINT('Ctrl Pts',(9.30913094759651,-2.51351000158156,4.));
#93724=CARTESIAN_POINT('Ctrl Pts',(9.28769420834347,-2.58354024740004,4.));
#93725=CARTESIAN_POINT('Ctrl Pts',(9.26547043733762,-2.65330301792625,4.));
#93726=CARTESIAN_POINT('Ctrl Pts',(9.19195458649819,-2.8840770585155,4.));
#93727=CARTESIAN_POINT('Ctrl Pts',(9.1098301701063,-3.11192550815888,4.));
#93728=CARTESIAN_POINT('Ctrl Pts',(9.01932452687049,-3.33637596952591,4.));
#93729=CARTESIAN_POINT('Ctrl Pts',(8.93690618262992,-3.54077024515911,4.));
#93730=CARTESIAN_POINT('Ctrl Pts',(8.84753676833139,-3.74234683886697,4.));
#93731=CARTESIAN_POINT('Ctrl Pts',(8.75135417901126,-3.94073274238285,4.));
#93732=CARTESIAN_POINT('Ctrl Pts',(8.67921723702116,-4.08952217001975,4.));
#93733=CARTESIAN_POINT('Ctrl Pts',(8.60324720993827,-4.23651654842593,4.));
#93734=CARTESIAN_POINT('Ctrl Pts',(8.5234913277534,-4.38155078557716,4.00000000000001));
#93735=CARTESIAN_POINT('Ctrl Pts',(8.49892468404568,-4.42622466206011,4.00000000000001));
#93736=CARTESIAN_POINT('Ctrl Pts',(8.47399670555403,-4.47071589760201,4.00000000000001));
#93737=CARTESIAN_POINT('Ctrl Pts',(8.44872637787968,-4.51498912509729,4.00000000000001));
#93738=CARTESIAN_POINT('Ctrl Pts',(8.32958796863387,-4.72371779549438,4.00000000000001));
#93739=CARTESIAN_POINT('Ctrl Pts',(8.2027667345669,-4.92774605616295,4.));
#93740=CARTESIAN_POINT('Ctrl Pts',(8.06846284138562,-5.12660291060759,4.00000000000001));
#93741=CARTESIAN_POINT('Ctrl Pts',(7.95380309505733,-5.29637368899813,4.00000000000001));
#93742=CARTESIAN_POINT('Ctrl Pts',(7.83368866631315,-5.46237506898967,4.));
#93743=CARTESIAN_POINT('Ctrl Pts',(7.70821968708721,-5.62429639443576,4.));
#93744=CARTESIAN_POINT('Ctrl Pts',(7.5607552682559,-5.81460346715293,4.));
#93745=CARTESIAN_POINT('Ctrl Pts',(7.40589473957772,-5.99927573772719,4.00000000000001));
#93746=CARTESIAN_POINT('Ctrl Pts',(7.24403667673219,-6.17797150278237,4.00000000000001));
#93747=CARTESIAN_POINT('Ctrl Pts',(7.22210427859886,-6.20218547516675,4.00000000000001));
#93748=CARTESIAN_POINT('Ctrl Pts',(7.20004334827914,-6.22628964950583,4.));
#93749=CARTESIAN_POINT('Ctrl Pts',(7.17785483368835,-6.25028311638451,4.));
#93750=CARTESIAN_POINT('Ctrl Pts',(7.17753992463812,-6.25025814508695,-2.77555756156289E-16));
#93751=CARTESIAN_POINT('Ctrl Pts',(7.33800998986773,-6.07641108632488,-1.70645015963758E-15));
#93752=CARTESIAN_POINT('Ctrl Pts',(7.49158121534325,-5.89679618497648,-2.48618949564423E-15));
#93753=CARTESIAN_POINT('Ctrl Pts',(7.63811298721216,-5.71192498565071,-2.14932238673526E-15));
#93754=CARTESIAN_POINT('Ctrl Pts',(7.78666634752559,-5.52450325768861,-1.2836841867506E-15));
#93755=CARTESIAN_POINT('Ctrl Pts',(7.92798505737963,-5.33167874732615,-3.99093992625071E-16));
#93756=CARTESIAN_POINT('Ctrl Pts',(8.06188982433472,-5.13394157588505,9.92261828258734E-16));
#93757=CARTESIAN_POINT('Ctrl Pts',(8.19685995208136,-4.93463118614655,2.15043722649999E-15));
#93758=CARTESIAN_POINT('Ctrl Pts',(8.32429807361849,-4.7303291359084,1.79060540631703E-15));
#93759=CARTESIAN_POINT('Ctrl Pts',(8.44398181039031,-4.52150145755031,7.63278329429795E-16));
#93760=CARTESIAN_POINT('Ctrl Pts',(8.56345030282558,-4.31304934379516,-7.43045306890748E-16));
#93761=CARTESIAN_POINT('Ctrl Pts',(8.67519260394167,-4.1000872941033,-3.85651484159796E-16));
#93762=CARTESIAN_POINT('Ctrl Pts',(8.77894385085711,-3.88305148407251,1.12410081243297E-15));
#93763=CARTESIAN_POINT('Ctrl Pts',(8.84287719073254,-3.74931020750599,1.05649064180309E-15));
#93764=CARTESIAN_POINT('Ctrl Pts',(8.90377525885169,-3.61402152351891,1.62340193009639E-15));
#93765=CARTESIAN_POINT('Ctrl Pts',(8.96156696082794,-3.47728373804748,1.06165076729781E-15));
#93766=CARTESIAN_POINT('Ctrl Pts',(9.00491073731013,-3.37473039894392,5.29634336720259E-16));
#93767=CARTESIAN_POINT('Ctrl Pts',(9.04650704156076,-3.27136187970652,-1.10473652131748E-15));
#93768=CARTESIAN_POINT('Ctrl Pts',(9.08632311880722,-3.16721890424697,2.22044604925031E-16));
#93769=CARTESIAN_POINT('Ctrl Pts',(9.09814351372692,-3.13630146628783,3.53555780382128E-16));
#93770=CARTESIAN_POINT('Ctrl Pts',(9.10980868158756,-3.10531118606065,-8.44808349090084E-16));
#93771=CARTESIAN_POINT('Ctrl Pts',(9.12131183370369,-3.07426508737355,-1.02695629777827E-15));
#93772=CARTESIAN_POINT('Ctrl Pts',(9.20591217134567,-2.84593546042613,-2.36656980581918E-15));
#93773=CARTESIAN_POINT('Ctrl Pts',(9.2816705280804,-2.61481991374847,-1.78377060807565E-16));
#93774=CARTESIAN_POINT('Ctrl Pts',(9.3483940664643,-2.38140358669778,-1.66533453693773E-15));
#93775=CARTESIAN_POINT('Ctrl Pts',(9.36427745395793,-2.32583935764635,-2.01930140308367E-15));
#93776=CARTESIAN_POINT('Ctrl Pts',(9.37964867883204,-2.27014461564336,-2.72027826337243E-15));
#93777=CARTESIAN_POINT('Ctrl Pts',(9.39450477735965,-2.21432566613214,-2.52575738102223E-15));
#93778=CARTESIAN_POINT('Ctrl Pts',(9.45650188159823,-1.98138340172106,-1.63274350975922E-15));
#93779=CARTESIAN_POINT('Ctrl Pts',(9.50953176974578,-1.74627967148825,-4.98055778690125E-16));
#93780=CARTESIAN_POINT('Ctrl Pts',(9.55366962715838,-1.50954126955344,-7.21644966006352E-16));
#93781=CARTESIAN_POINT('Ctrl Pts',(9.59810773930183,-1.27119241733133,-9.4675515400523E-16));
#93782=CARTESIAN_POINT('Ctrl Pts',(9.63353251352791,-1.03118594416952,-4.86217381181644E-15));
#93783=CARTESIAN_POINT('Ctrl Pts',(9.65996981531948,-0.790043545297951,
-3.81639164714898E-15));
#93784=CARTESIAN_POINT('Ctrl Pts',(9.68639436464155,-0.549017465448327,
-2.77111393279442E-15));
#93785=CARTESIAN_POINT('Ctrl Pts',(9.703840143681,-0.306855896272764,-4.36666804480211E-15));
#93786=CARTESIAN_POINT('Ctrl Pts',(9.71228155096646,-0.064073667508046,
-4.3159920082303E-15));
#93787=CARTESIAN_POINT('Ctrl Pts',(9.71962495034288,0.147128897067642,-4.27190760822724E-15));
#93788=CARTESIAN_POINT('Ctrl Pts',(9.72015333295581,0.358801518323463,-3.13158552209261E-15));
#93789=CARTESIAN_POINT('Ctrl Pts',(9.71381780952735,0.570603154075694,-1.52655665885959E-16));
#93790=CARTESIAN_POINT('Ctrl Pts',(9.71299313018453,0.598172846738271,3.49337317364136E-16));
#93791=CARTESIAN_POINT('Ctrl Pts',(9.71205204699908,0.625745335211232,-3.50308968122191E-15));
#93792=CARTESIAN_POINT('Ctrl Pts',(9.71099513918219,0.653304042026428,-3.38618022510673E-15));
#93793=CARTESIAN_POINT('Ctrl Pts',(9.70161065125207,0.898003104086462,-2.15789795742488E-15));
#93794=CARTESIAN_POINT('Ctrl Pts',(9.68309081241473,1.14191242342517,1.50994968166066E-15));
#93795=CARTESIAN_POINT('Ctrl Pts',(9.65550811589912,1.3845043278793,1.80411241501588E-15));
#93796=CARTESIAN_POINT('Ctrl Pts',(9.62779434503325,1.62824904116905,1.60411412740023E-15));
#93797=CARTESIAN_POINT('Ctrl Pts',(9.59093142972806,1.87066445397657,1.89804298519407E-15));
#93798=CARTESIAN_POINT('Ctrl Pts',(9.54494106673758,2.11122282572072,2.16493489801906E-15));
#93799=CARTESIAN_POINT('Ctrl Pts',(9.52299473622331,2.22601586476162,2.79879565106048E-15));
#93800=CARTESIAN_POINT('Ctrl Pts',(9.49896919359987,2.34038607617966,1.28207721328556E-15));
#93801=CARTESIAN_POINT('Ctrl Pts',(9.47286261042038,2.45427603255219,2.1094237467878E-15));
#93802=CARTESIAN_POINT('Ctrl Pts',(9.41829613481954,2.69232225571569,3.98098628479859E-15));
#93803=CARTESIAN_POINT('Ctrl Pts',(9.35464154134197,2.9282712247136,3.88869133735323E-15));
#93804=CARTESIAN_POINT('Ctrl Pts',(9.28216391978015,3.16167853502839,2.77555756156289E-15));
#93805=CARTESIAN_POINT('Ctrl Pts',(9.20955144462212,3.39552012856739,1.37319592695381E-15));
#93806=CARTESIAN_POINT('Ctrl Pts',(9.12808282575743,3.62681119853611,2.89145976353516E-15));
#93807=CARTESIAN_POINT('Ctrl Pts',(9.03797511128659,3.8550881756909,3.05311331771918E-15));
#93808=CARTESIAN_POINT('Ctrl Pts',(8.98726023624883,3.98356816698121,4.01994859505052E-15));
#93809=CARTESIAN_POINT('Ctrl Pts',(8.93380786638176,4.11109302736784,6.30449953712883E-15));
#93810=CARTESIAN_POINT('Ctrl Pts',(8.87765027447099,4.23757668725412,4.02455846426619E-15));
#93811=CARTESIAN_POINT('Ctrl Pts',(8.86122693757481,4.27456694427003,2.69626927025734E-15));
#93812=CARTESIAN_POINT('Ctrl Pts',(8.84457022494813,4.31147221868278,1.27775149067983E-16));
#93813=CARTESIAN_POINT('Ctrl Pts',(8.82769617356933,4.34825761285522,3.88578058618805E-16));
#93814=CARTESIAN_POINT('Ctrl Pts',(8.72485940884878,4.57244152937544,1.97800829358891E-15));
#93815=CARTESIAN_POINT('Ctrl Pts',(8.61384827011246,4.79241862612696,3.30332224731784E-15));
#93816=CARTESIAN_POINT('Ctrl Pts',(8.49498716931974,5.0077596047636,2.4980018054066E-15));
#93817=CARTESIAN_POINT('Ctrl Pts',(8.37548437725773,5.22426313721297,1.68833370818081E-15));
#93818=CARTESIAN_POINT('Ctrl Pts',(8.2480463831814,5.43608096212101,-1.79289508799685E-15));
#93819=CARTESIAN_POINT('Ctrl Pts',(8.11295156724744,5.64276359635317,-3.13638004456607E-15));
#93820=CARTESIAN_POINT('Ctrl Pts',(7.97823586637413,5.84886621943632,-4.47609479443058E-15));
#93821=CARTESIAN_POINT('Ctrl Pts',(7.83590594907037,6.04986301653102,-4.53666372321089E-15));
#93822=CARTESIAN_POINT('Ctrl Pts',(7.68619128271507,6.24528632274246,-4.71844785465692E-15));
#93823=CARTESIAN_POINT('Ctrl Pts',(7.57338197961842,6.39253687286717,-4.85542135018466E-15));
#93824=CARTESIAN_POINT('Ctrl Pts',(7.45637896929152,6.53662265622548,-5.76567150700508E-15));
#93825=CARTESIAN_POINT('Ctrl Pts',(7.33526444267627,6.6773322800225,-7.105427357601E-15));
#93826=CARTESIAN_POINT('Ctrl Pts',(7.20393068439424,6.82991450311471,-8.37772598309406E-15));
#93827=CARTESIAN_POINT('Ctrl Pts',(7.06776233301774,6.97852710790817,-7.71770923598613E-15));
#93828=CARTESIAN_POINT('Ctrl Pts',(6.92698202333213,7.12300579317397,-7.66053886991358E-15));
#93829=CARTESIAN_POINT('Ctrl Pts',(6.86539063784465,7.18621521797778,-6.99661795502185E-15));
#93830=CARTESIAN_POINT('Ctrl Pts',(6.80291629536247,7.24863316335114,-9.1940653235129E-15));
#93831=CARTESIAN_POINT('Ctrl Pts',(6.73957677015636,7.31024478793457,-8.65973959207622E-15));
#93832=CARTESIAN_POINT('Ctrl Pts',(6.71407214296748,7.33505364954804,-8.43710487480707E-15));
#93833=CARTESIAN_POINT('Ctrl Pts',(6.68842723008856,7.3597317670364,-8.81881235844313E-15));
#93834=CARTESIAN_POINT('Ctrl Pts',(6.66264317018596,7.38427813926213,-9.52016243616072E-15));
#93835=CARTESIAN_POINT('Ctrl Pts',(6.64018129830422,7.40566179529529,-1.01311459526996E-14));
#93836=CARTESIAN_POINT('Ctrl Pts',(6.6176136785009,7.42694554332174,-1.02041435804245E-14));
#93837=CARTESIAN_POINT('Ctrl Pts',(6.59495234791835,7.44811834977477,-9.38138455808257E-15));
#93838=CARTESIAN_POINT('Ctrl Pts',(6.41390316478046,7.61727520043247,-2.80807905990282E-15));
#93839=CARTESIAN_POINT('Ctrl Pts',(6.22670570529577,7.77951654972426,-8.71920794202464E-15));
#93840=CARTESIAN_POINT('Ctrl Pts',(6.03383377828811,7.93459536759427,-9.27036225562006E-15));
#93841=CARTESIAN_POINT('Ctrl Pts',(5.83693737649259,8.09291006744219,-9.83301698129566E-15));
#93842=CARTESIAN_POINT('Ctrl Pts',(5.63412705071208,8.2437605256776,-1.02724545597727E-14));
#93843=CARTESIAN_POINT('Ctrl Pts',(5.42586725408438,8.38684523466999,-1.12132525487141E-14));
#93844=CARTESIAN_POINT('Ctrl Pts',(5.2696724066136,8.49415876641429,-1.19188510404201E-14));
#93845=CARTESIAN_POINT('Ctrl Pts',(5.11041134210566,8.59710331969617,-1.08867618319524E-14));
#93846=CARTESIAN_POINT('Ctrl Pts',(4.9482678399785,8.6955353474984,-1.12687636999453E-14));
#93847=CARTESIAN_POINT('Ctrl Pts',(4.8988306515854,8.72554705094956,-1.13852352086196E-14));
#93848=CARTESIAN_POINT('Ctrl Pts',(4.84912544012257,8.75513915261243,-1.12031239875748E-14));
#93849=CARTESIAN_POINT('Ctrl Pts',(4.79915725517255,8.78430729888448,-1.0769163338864E-14));
#93850=CARTESIAN_POINT('Ctrl Pts',(4.75991955858719,8.80721169043932,-1.04283941818269E-14));
#93851=CARTESIAN_POINT('Ctrl Pts',(4.72052094035713,8.82985381860244,-1.24133512762974E-14));
#93852=CARTESIAN_POINT('Ctrl Pts',(4.6809837830536,8.85222064328245,-1.21014309684142E-14));
#93853=CARTESIAN_POINT('Ctrl Pts',(4.46299776725799,8.97553894258666,-1.03816749262894E-14));
#93854=CARTESIAN_POINT('Ctrl Pts',(4.24064629173592,9.09058407405512,-1.0004645565113E-14));
#93855=CARTESIAN_POINT('Ctrl Pts',(4.01438138172824,9.19707375790166,-8.43769498715119E-15));
#93856=CARTESIAN_POINT('Ctrl Pts',(3.81972423991358,9.28868751051407,-7.08963743434491E-15));
#93857=CARTESIAN_POINT('Ctrl Pts',(3.6221698828145,9.37396868113959,-6.94744677900428E-15));
#93858=CARTESIAN_POINT('Ctrl Pts',(3.42198926643324,9.45271166426703,-6.21724893790088E-15));
#93859=CARTESIAN_POINT('Ctrl Pts',(3.18987041866164,9.54401785986204,-5.32066284343393E-15));
#93860=CARTESIAN_POINT('Ctrl Pts',(2.95422040193964,9.62653437420915,-2.00867961754982E-15));
#93861=CARTESIAN_POINT('Ctrl Pts',(2.71555643549459,9.70021149728078,-1.4432899320127E-15));
#93862=CARTESIAN_POINT('Ctrl Pts',(2.67798368606114,9.71181045009038,-1.35428091526265E-15));
#93863=CARTESIAN_POINT('Ctrl Pts',(2.64033620760127,9.72319022676346,-2.52363653881751E-15));
#93864=CARTESIAN_POINT('Ctrl Pts',(2.60261598667549,9.73435052034593,9.99200722162641E-16));
#93865=CARTESIAN_POINT('Ctrl Pts',(-2.60250042474766,9.73470771305938,0.000337104101208169));
#93866=CARTESIAN_POINT('Ctrl Pts',(-4.17620603742513,9.31398942894217,0.026065973894913));
#93867=CARTESIAN_POINT('Ctrl Pts',(-7.11443254118295,7.6957742419676,0.0775237134823225));
#93868=CARTESIAN_POINT('Ctrl Pts',(-9.88170779441914,3.49088825292512,0.154710322863437));
#93869=CARTESIAN_POINT('Ctrl Pts',(-10.3696118635881,-1.51802545263044,
0.231896932244551));
#93870=CARTESIAN_POINT('Ctrl Pts',(-8.46615891068372,-6.1773600095809,0.309083541625665));
#93871=CARTESIAN_POINT('Ctrl Pts',(-4.61007004150353,-9.41175154011344,
0.38627015100678));
#93872=CARTESIAN_POINT('Ctrl Pts',(0.309190375968473,-10.4756492852767,
0.463456760387894));
#93873=CARTESIAN_POINT('Ctrl Pts',(5.15716569486616,-9.1234875171854,0.540643369769009));
#93874=CARTESIAN_POINT('Ctrl Pts',(8.81573533404148,-5.66721546296529,0.617829979150123));
#93875=CARTESIAN_POINT('Ctrl Pts',(10.4411434074219,-0.90389988182744,0.695016588531238));
#93876=CARTESIAN_POINT('Ctrl Pts',(9.65851409104835,4.06787287683326,0.772203197912351));
#93877=CARTESIAN_POINT('Ctrl Pts',(6.64834923647149,8.1014790533001,0.849389807293467));
#93878=CARTESIAN_POINT('Ctrl Pts',(2.10487898349287,10.2666439587759,0.92657641667458));
#93879=CARTESIAN_POINT('Ctrl Pts',(-2.92403780237063,10.064020314243,1.0037630260557));
#93880=CARTESIAN_POINT('Ctrl Pts',(-7.27858577628976,7.54033738966125,1.08094963543681));
#93881=CARTESIAN_POINT('Ctrl Pts',(-9.95447796485031,3.27763145687328,1.15813624481793));
#93882=CARTESIAN_POINT('Ctrl Pts',(-10.3345751767764,-1.74099271462887,
1.23532285419904));
#93883=CARTESIAN_POINT('Ctrl Pts',(-8.33121575360925,-6.35809275148398,
1.31250946358015));
#93884=CARTESIAN_POINT('Ctrl Pts',(-4.40643326471,-9.5088298708975,1.38969607296127));
#93885=CARTESIAN_POINT('Ctrl Pts',(0.534602178678755,-10.4665514853921,
1.46688268234238));
#93886=CARTESIAN_POINT('Ctrl Pts',(5.35234265263788,-9.01037888642927,1.5440692917235));
#93887=CARTESIAN_POINT('Ctrl Pts',(8.9356756897984,-5.47614823539465,1.62125590110461));
#93888=CARTESIAN_POINT('Ctrl Pts',(10.4581794303881,-0.678956944208766,
1.69844251048573));
#93889=CARTESIAN_POINT('Ctrl Pts',(9.56871979020855,4.27482176361841,1.77562911986684));
#93890=CARTESIAN_POINT('Ctrl Pts',(6.47243228913536,8.24270100106766,1.85281572924795));
#93891=CARTESIAN_POINT('Ctrl Pts',(1.88341177736483,10.3095712621668,1.93000233862907));
#93892=CARTESIAN_POINT('Ctrl Pts',(-3.13997881473699,9.99875155080307,2.00718894801018));
#93893=CARTESIAN_POINT('Ctrl Pts',(-7.439198056598,7.38192602284617,2.0843755573913));
#93894=CARTESIAN_POINT('Ctrl Pts',(-10.0227197033554,3.06261151306865,2.16156216677241));
#93895=CARTESIAN_POINT('Ctrl Pts',(-10.2947077734096,-1.96303117452732,
2.23874877615352));
#93896=CARTESIAN_POINT('Ctrl Pts',(-8.19243382826692,-6.53594121004401,
2.31593538553464));
#93897=CARTESIAN_POINT('Ctrl Pts',(-4.20074399310361,-9.60147121212246,
2.39312199491575));
#93898=CARTESIAN_POINT('Ctrl Pts',(0.759760801971393,-10.4526199134108,
2.47030860429687));
#93899=CARTESIAN_POINT('Ctrl Pts',(5.54504243837757,-8.89308742174652,2.54749521367798));
#93900=CARTESIAN_POINT('Ctrl Pts',(9.0514744054115,-5.28254773934542,2.6246818230591));
#93901=CARTESIAN_POINT('Ctrl Pts',(10.4703704910301,-0.453697376934528,
2.70186843244021));
#93902=CARTESIAN_POINT('Ctrl Pts',(9.47449157942137,4.47978893026564,2.77905504182133));
#93903=CARTESIAN_POINT('Ctrl Pts',(6.29351659914733,8.38010431331672,2.85624165120244));
#93904=CARTESIAN_POINT('Ctrl Pts',(1.66107182433835,10.347721489507,2.93342826058356));
#93905=CARTESIAN_POINT('Ctrl Pts',(-3.3544649115547,9.92885011100522,3.01061486996467));
#93906=CARTESIAN_POINT('Ctrl Pts',(-7.5963634927572,7.22009427935256,3.08780147934578));
#93907=CARTESIAN_POINT('Ctrl Pts',(-10.0863175325862,2.84617254424586,3.1649880887269));
#93908=CARTESIAN_POINT('Ctrl Pts',(-10.2500704286301,-2.18416003554074,
3.24217469810801));
#93909=CARTESIAN_POINT('Ctrl Pts',(-8.04985607047069,-6.71076144710083,
3.31936130748913));
#93910=CARTESIAN_POINT('Ctrl Pts',(-3.99310828706469,-9.68966356068127,
3.39654791687024));
#93911=CARTESIAN_POINT('Ctrl Pts',(0.984567258195362,-10.4338457787741,
3.47373452625136));
#93912=CARTESIAN_POINT('Ctrl Pts',(5.7351732752715,-8.77167439498682,3.55092113563247));
#93913=CARTESIAN_POINT('Ctrl Pts',(9.16307867541303,-5.08650172897933,3.62810774501358));
#93914=CARTESIAN_POINT('Ctrl Pts',(10.4777113261985,-0.228223461525968,
3.7052943543947));
#93915=CARTESIAN_POINT('Ctrl Pts',(9.37587131291801,4.68267227169952,3.78248096377581));
#93916=CARTESIAN_POINT('Ctrl Pts',(6.11168916100159,8.51364095061604,3.85966757315693));
#93917=CARTESIAN_POINT('Ctrl Pts',(1.43795377928683,10.3810453119631,3.93685418253804));
#93918=CARTESIAN_POINT('Ctrl Pts',(-3.56738003678192,9.85441135035922,4.01404079191916));
#93919=CARTESIAN_POINT('Ctrl Pts',(-7.75004242324465,7.05479226584377,4.09122740130027));
#93920=CARTESIAN_POINT('Ctrl Pts',(-10.1451748614197,2.62866444414504,4.16841401068139));
#93921=CARTESIAN_POINT('Ctrl Pts',(-10.2008382774016,-2.40515970586688,
4.24560611132689));
#93922=CARTESIAN_POINT('Ctrl Pts',(-8.66860765197138,-5.38957635420927,
4.29706934217869));
#93923=CARTESIAN_POINT('Ctrl Pts',(-7.59848317952396,-6.61820187589613,
4.32280370323678));
#93924=CARTESIAN_POINT('Ctrl Pts',(-2.5542913309526,9.55438058121967,-0.107431152205371));
#93925=CARTESIAN_POINT('Ctrl Pts',(-4.09884539354156,9.14145574336953,-0.0817022824116669));
#93926=CARTESIAN_POINT('Ctrl Pts',(-6.98264376512165,7.55321660826708,-0.0302445428242573));
#93927=CARTESIAN_POINT('Ctrl Pts',(-9.69865761183838,3.42622253467468,0.0469420665568571));
#93928=CARTESIAN_POINT('Ctrl Pts',(-10.1775236755531,-1.48990532986955,
0.124128675937972));
#93929=CARTESIAN_POINT('Ctrl Pts',(-8.30933056009907,-6.06292970045364,
0.201315285319086));
#93930=CARTESIAN_POINT('Ctrl Pts',(-4.52467243813745,-9.23740689507186,
0.278501894700201));
#93931=CARTESIAN_POINT('Ctrl Pts',(0.303462888781973,-10.2815968447254,
0.355688504081315));
#93932=CARTESIAN_POINT('Ctrl Pts',(5.0616336125901,-8.95448271654383,0.432875113462429));
#93933=CARTESIAN_POINT('Ctrl Pts',(8.65243137929479,-5.56223514510909,0.510061722843545));
#93934=CARTESIAN_POINT('Ctrl Pts',(10.2477301587364,-0.887155909849574,
0.587248332224658));
#93935=CARTESIAN_POINT('Ctrl Pts',(9.47959838086883,3.99251901206505,0.664434941605773));
#93936=CARTESIAN_POINT('Ctrl Pts',(6.52519425487164,7.95140608507103,0.741621550986887));
#93937=CARTESIAN_POINT('Ctrl Pts',(2.06588790115624,10.0764631630832,0.818808160368001));
#93938=CARTESIAN_POINT('Ctrl Pts',(-2.86987250374691,9.87759294821029,0.895994769749116));
#93939=CARTESIAN_POINT('Ctrl Pts',(-7.14375620198966,7.40065909066546,0.97318137913023));
#93940=CARTESIAN_POINT('Ctrl Pts',(-9.77007977712095,3.21691613831752,1.05036798851134));
#93941=CARTESIAN_POINT('Ctrl Pts',(-10.1431360133889,-1.70874231409945,
1.12755459789246));
#93942=CARTESIAN_POINT('Ctrl Pts',(-8.17688710955856,-6.24031452293913,
1.20474120727357));
#93943=CARTESIAN_POINT('Ctrl Pts',(-4.32480785841224,-9.33268693283367,
1.28192781665468));
#93944=CARTESIAN_POINT('Ctrl Pts',(0.524699130698473,-10.2726675738001,
1.3591144260358));
#93945=CARTESIAN_POINT('Ctrl Pts',(5.25319508420306,-8.84346932640218,1.43630103541691));
#93946=CARTESIAN_POINT('Ctrl Pts',(8.77014994257647,-5.37470727446133,1.51348764479803));
#93947=CARTESIAN_POINT('Ctrl Pts',(10.2644506039523,-0.666379847699995,
1.59067425417914));
#93948=CARTESIAN_POINT('Ctrl Pts',(9.39146744262841,4.19563434777797,1.66786086356025));
#93949=CARTESIAN_POINT('Ctrl Pts',(6.3525360184789,8.09001201707886,1.74504747294137));
#93950=CARTESIAN_POINT('Ctrl Pts',(1.84852318554509,10.1185952749053,1.82223408232248));
#93951=CARTESIAN_POINT('Ctrl Pts',(-3.08181339360786,9.81353323277227,1.8994206917036));
#93952=CARTESIAN_POINT('Ctrl Pts',(-7.30139327721728,7.24518215889154,1.97660730108471));
#93953=CARTESIAN_POINT('Ctrl Pts',(-9.83705739580452,3.00587925501121,2.05379391046583));
#93954=CARTESIAN_POINT('Ctrl Pts',(-10.1040071195608,-1.92666770149365,
2.13098051984694));
#93955=CARTESIAN_POINT('Ctrl Pts',(-8.04067600064811,-6.41486849096287,
2.20816712922805));
#93956=CARTESIAN_POINT('Ctrl Pts',(-4.12292880458458,-9.42361217247189,
2.28535373860917));
#93957=CARTESIAN_POINT('Ctrl Pts',(0.745686883129435,-10.2589940722704,
2.36254034799028));
#93958=CARTESIAN_POINT('Ctrl Pts',(5.44232527127653,-8.72835058575378,2.4397269573714));
#93959=CARTESIAN_POINT('Ctrl Pts',(8.88380358605459,-5.18469306196619,2.51691356675251));
#93960=CARTESIAN_POINT('Ctrl Pts',(10.2764158356259,-0.445293021188328,
2.59410017613363));
#93961=CARTESIAN_POINT('Ctrl Pts',(9.29898472882896,4.39680467302303,2.67128678551474));
#93962=CARTESIAN_POINT('Ctrl Pts',(6.17693458857629,8.22487005052414,2.74847339489586));
#93963=CARTESIAN_POINT('Ctrl Pts',(1.63030188992512,10.1560388019235,2.82566000427697));
#93964=CARTESIAN_POINT('Ctrl Pts',(-3.29232631898595,9.74492665734239,2.90284661365808));
#93965=CARTESIAN_POINT('Ctrl Pts',(-7.45564735813477,7.08634820999072,2.9800332230392));
#93966=CARTESIAN_POINT('Ctrl Pts',(-9.89947712966015,2.79344963291115,3.05721983242031));
#93967=CARTESIAN_POINT('Ctrl Pts',(-10.0601966434038,-2.14370033954394,
3.13440644180143));
#93968=CARTESIAN_POINT('Ctrl Pts',(-7.90073937383241,-6.58645033269596,
3.21159305118254));
#93969=CARTESIAN_POINT('Ctrl Pts',(-3.91913937235699,-9.51017083322676,
3.28877966056366));
#93970=CARTESIAN_POINT('Ctrl Pts',(0.96632899208538,-10.2405677124156,3.36596626994477));
#93971=CARTESIAN_POINT('Ctrl Pts',(5.62893409708374,-8.60918663143969,3.44315287932589));
#93972=CARTESIAN_POINT('Ctrl Pts',(8.99334048243757,-4.99227863621464,3.520339488707));
#93973=CARTESIAN_POINT('Ctrl Pts',(10.2836206881034,-0.223995817158145,
3.59752609808812));
#93974=CARTESIAN_POINT('Ctrl Pts',(9.20219131838785,4.59592977413402,3.67471270746923));
#93975=CARTESIAN_POINT('Ctrl Pts',(5.99847534815945,8.35593303586498,3.75189931685034));
#93976=CARTESIAN_POINT('Ctrl Pts',(1.41131691576919,10.1887453290789,3.82908592623146));
#93977=CARTESIAN_POINT('Ctrl Pts',(-3.50129737367821,9.67186681105117,3.90627253561257));
#93978=CARTESIAN_POINT('Ctrl Pts',(-7.6064795179152,6.92410827485778,3.98345914499369));
#93979=CARTESIAN_POINT('Ctrl Pts',(-9.95724417683243,2.57997068427531,4.0606457543748));
#93980=CARTESIAN_POINT('Ctrl Pts',(-10.0118764756561,-2.36060618005391,
4.13783785502032));
#93981=CARTESIAN_POINT('Ctrl Pts',(-8.50802911165971,-5.28973906330818,
4.18930108587212));
#93982=CARTESIAN_POINT('Ctrl Pts',(-7.45772777951767,-6.49560534835832,
4.21503544693021));
#93983=CARTESIAN_POINT('Ctrl Pts',(-2.50608223715753,9.37405344937994,-0.215199408511951));
#93984=CARTESIAN_POINT('Ctrl Pts',(-4.02148474965799,8.96892205779688,-0.189470538718247));
#93985=CARTESIAN_POINT('Ctrl Pts',(-6.85085498906034,7.41065897456655,-0.138012799130837));
#93986=CARTESIAN_POINT('Ctrl Pts',(-9.51560742925762,3.36155681642425,-0.0608261897497226));
#93987=CARTESIAN_POINT('Ctrl Pts',(-9.9854354875181,-1.46178520710867,0.0163604196313919));
#93988=CARTESIAN_POINT('Ctrl Pts',(-8.15250220951439,-5.94849939132635,
0.093547029012506));
#93989=CARTESIAN_POINT('Ctrl Pts',(-4.43927483477137,-9.06306225003029,
0.170733638393621));
#93990=CARTESIAN_POINT('Ctrl Pts',(0.297735401595483,-10.0875444041741,
0.247920247774735));
#93991=CARTESIAN_POINT('Ctrl Pts',(4.96610153031403,-8.78547791590226,0.32510685715585));
#93992=CARTESIAN_POINT('Ctrl Pts',(8.4891274245481,-5.45725482725287,0.402293466536964));
#93993=CARTESIAN_POINT('Ctrl Pts',(10.0543169100508,-0.870411937871706,
0.479480075918078));
#93994=CARTESIAN_POINT('Ctrl Pts',(9.30068267068929,3.91716514729685,0.556666685299193));
#93995=CARTESIAN_POINT('Ctrl Pts',(6.40203927327179,7.80133311684196,0.633853294680306));
#93996=CARTESIAN_POINT('Ctrl Pts',(2.0268968188196,9.88628236739044,0.711039904061421));
#93997=CARTESIAN_POINT('Ctrl Pts',(-2.81570720512321,9.69116558217758,0.788226513442536));
#93998=CARTESIAN_POINT('Ctrl Pts',(-7.00892662768955,7.26098079166965,0.86541312282365));
#93999=CARTESIAN_POINT('Ctrl Pts',(-9.58568158939161,3.15620081976177,0.942599732204765));
#94000=CARTESIAN_POINT('Ctrl Pts',(-9.95169685000138,-1.67649191357006,
1.01978634158588));
#94001=CARTESIAN_POINT('Ctrl Pts',(-8.02255846550788,-6.12253629439428,
1.09697295096699));
#94002=CARTESIAN_POINT('Ctrl Pts',(-4.24318245211449,-9.15654399476985,
1.17415956034811));
#94003=CARTESIAN_POINT('Ctrl Pts',(0.514796082718195,-10.078783662208,1.25134616972922));
#94004=CARTESIAN_POINT('Ctrl Pts',(5.15404751576823,-8.6765597663751,1.32853277911034));
#94005=CARTESIAN_POINT('Ctrl Pts',(8.60462419535454,-5.27326631352799,1.40571938849145));
#94006=CARTESIAN_POINT('Ctrl Pts',(10.0707217775164,-0.653802751191223,
1.48290599787256));
#94007=CARTESIAN_POINT('Ctrl Pts',(9.21421509504826,4.11644693193751,1.56009260725368));
#94008=CARTESIAN_POINT('Ctrl Pts',(6.23263974782243,7.93732303309007,1.63727921663479));
#94009=CARTESIAN_POINT('Ctrl Pts',(1.81363459372535,9.92761928764379,1.71446582601591));
#94010=CARTESIAN_POINT('Ctrl Pts',(-3.02364797247873,9.62831491474147,1.79165243539702));
#94011=CARTESIAN_POINT('Ctrl Pts',(-7.16358849783658,7.10843829493689,1.86883904477814));
#94012=CARTESIAN_POINT('Ctrl Pts',(-9.65139508825367,2.94914699695377,1.94602565415925));
#94013=CARTESIAN_POINT('Ctrl Pts',(-9.91330646571203,-1.89030422845998,
2.02321226354037));
#94014=CARTESIAN_POINT('Ctrl Pts',(-7.88891817302927,-6.29379577188174,
2.10039887292148));
#94015=CARTESIAN_POINT('Ctrl Pts',(-4.04511361606556,-9.24575313282132,
2.17758548230259));
#94016=CARTESIAN_POINT('Ctrl Pts',(0.731612964287487,-10.0653682311302,
2.25477209168371));
#94017=CARTESIAN_POINT('Ctrl Pts',(5.33960810417548,-8.56361374976105,2.33195870106482));
#94018=CARTESIAN_POINT('Ctrl Pts',(8.71613276669772,-5.08683838458696,2.40914531044594));
#94019=CARTESIAN_POINT('Ctrl Pts',(10.0824611802217,-0.436888665442129,
2.48633191982705));
#94020=CARTESIAN_POINT('Ctrl Pts',(9.12347787823656,4.31382041578043,2.56351852920817));
#94021=CARTESIAN_POINT('Ctrl Pts',(6.06035257800524,8.06963578773155,2.64070513858928));
#94022=CARTESIAN_POINT('Ctrl Pts',(1.5995319555119,9.96435611433997,2.7178917479704));
#94023=CARTESIAN_POINT('Ctrl Pts',(-3.2301877264172,9.56100320367956,2.79507835735151));
#94024=CARTESIAN_POINT('Ctrl Pts',(-7.31493122351235,6.95260214062888,2.87226496673263));
#94025=CARTESIAN_POINT('Ctrl Pts',(-9.71263672673402,2.74072672157646,2.94945157611374));
#94026=CARTESIAN_POINT('Ctrl Pts',(-9.87032285817758,-2.10324064354715,
3.02663818549485));
#94027=CARTESIAN_POINT('Ctrl Pts',(-7.75162267719414,-6.46213921829106,
3.10382479487597));
#94028=CARTESIAN_POINT('Ctrl Pts',(-3.84517045764928,-9.33067810577225,
3.18101140425708));
#94029=CARTESIAN_POINT('Ctrl Pts',(0.948090725975405,-10.0472896460573,
3.2581980136382));
#94030=CARTESIAN_POINT('Ctrl Pts',(5.52269491889597,-8.44669886789258,3.33538462301931));
#94031=CARTESIAN_POINT('Ctrl Pts',(8.82360228946212,-4.89805554344996,3.41257123240042));
#94032=CARTESIAN_POINT('Ctrl Pts',(10.0895300500082,-0.219768172790326,
3.48975784178154));
#94033=CARTESIAN_POINT('Ctrl Pts',(9.02851132385769,4.50918727656851,3.56694445116265));
#94034=CARTESIAN_POINT('Ctrl Pts',(5.88526153531729,8.19822512111389,3.64413106054377));
#94035=CARTESIAN_POINT('Ctrl Pts',(1.38468005225154,9.99644534619459,3.72131766992488));
#94036=CARTESIAN_POINT('Ctrl Pts',(-3.43521471057451,9.48932227174309,3.798504279306));
#94037=CARTESIAN_POINT('Ctrl Pts',(-7.46291661258574,6.79342428387181,3.87569088868711));
#94038=CARTESIAN_POINT('Ctrl Pts',(-9.76931349224516,2.53127692440558,3.95287749806823));
#94039=CARTESIAN_POINT('Ctrl Pts',(-9.82291467391069,-2.31605265424095,
4.03006959871373));
#94040=CARTESIAN_POINT('Ctrl Pts',(-8.34745057134804,-5.1899017724071,4.08153282956553));
#94041=CARTESIAN_POINT('Ctrl Pts',(-7.3169723795114,-6.37300882082051,4.10726719062362));
#94042=CARTESIAN_POINT('Ctrl Pts',(-2.45787314336247,9.19372631754022,-0.322967664818532));
#94043=CARTESIAN_POINT('Ctrl Pts',(-3.94412410577443,8.79638837222423,-0.297238795024827));
#94044=CARTESIAN_POINT('Ctrl Pts',(-6.71906621299902,7.26810134086602,-0.245781055437418));
#94045=CARTESIAN_POINT('Ctrl Pts',(-9.33255724667688,3.29689109817383,-0.168594446056303));
#94046=CARTESIAN_POINT('Ctrl Pts',(-9.79334729948307,-1.43366508434778,
-0.0914078366751879));
#94047=CARTESIAN_POINT('Ctrl Pts',(-7.99567385892974,-5.83406908219907,
-0.0142212272940741));
#94048=CARTESIAN_POINT('Ctrl Pts',(-4.3538772314053,-8.88871760498874,0.062965382087041));
#94049=CARTESIAN_POINT('Ctrl Pts',(0.292007914408984,-9.89349196362283,
0.140151991468154));
#94050=CARTESIAN_POINT('Ctrl Pts',(4.87056944803797,-8.6164731152607,0.21733860084927));
#94051=CARTESIAN_POINT('Ctrl Pts',(8.32582346980139,-5.35227450939667,0.294525210230383));
#94052=CARTESIAN_POINT('Ctrl Pts',(9.86090366136514,-0.85366796589384,0.371711819611499));
#94053=CARTESIAN_POINT('Ctrl Pts',(9.12176696050975,3.84181128252864,0.448898428992612));
#94054=CARTESIAN_POINT('Ctrl Pts',(6.27888429167194,7.6512601486129,0.526085038373727));
#94055=CARTESIAN_POINT('Ctrl Pts',(1.98790573648296,9.69610157169772,0.603271647754841));
#94056=CARTESIAN_POINT('Ctrl Pts',(-2.76154190649949,9.50473821614484,0.680458257135956));
#94057=CARTESIAN_POINT('Ctrl Pts',(-6.87409705338946,7.12130249267385,0.75764486651707));
#94058=CARTESIAN_POINT('Ctrl Pts',(-9.40128340166224,3.09548550120601,0.834831475898185));
#94059=CARTESIAN_POINT('Ctrl Pts',(-9.76025768661387,-1.64424151304064,
0.912018085279298));
#94060=CARTESIAN_POINT('Ctrl Pts',(-7.86822982145718,-6.00475806584942,
0.989204694660414));
#94061=CARTESIAN_POINT('Ctrl Pts',(-4.16155704581674,-8.98040105670602,
1.06639130404152));
#94062=CARTESIAN_POINT('Ctrl Pts',(0.504893034737917,-9.88489975061589,
1.14357791342264));
#94063=CARTESIAN_POINT('Ctrl Pts',(5.0548999473334,-8.50965020634803,1.22076452280375));
#94064=CARTESIAN_POINT('Ctrl Pts',(8.43909844813259,-5.17182535259465,1.29795113218487));
#94065=CARTESIAN_POINT('Ctrl Pts',(9.87699295108057,-0.641225654682458,
1.37513774156598));
#94066=CARTESIAN_POINT('Ctrl Pts',(9.03696274746812,4.03725951609706,1.45232435094709));
#94067=CARTESIAN_POINT('Ctrl Pts',(6.11274347716597,7.78463404910127,1.52951096032821));
#94068=CARTESIAN_POINT('Ctrl Pts',(1.77874600190563,9.73664330038228,1.60669756970932));
#94069=CARTESIAN_POINT('Ctrl Pts',(-2.96548255134962,9.44309659671067,1.68388417909044));
#94070=CARTESIAN_POINT('Ctrl Pts',(-7.02578371845584,6.97169443098224,1.76107078847155));
#94071=CARTESIAN_POINT('Ctrl Pts',(-9.46573278070284,2.89241473889634,1.83825739785267));
#94072=CARTESIAN_POINT('Ctrl Pts',(-9.72260581186326,-1.85394075542631,
1.91544400723378));
#94073=CARTESIAN_POINT('Ctrl Pts',(-7.73716034541045,-6.17272305280058,
1.9926306166149));
#94074=CARTESIAN_POINT('Ctrl Pts',(-3.96729842754654,-9.06789409317076,
2.06981722599601));
#94075=CARTESIAN_POINT('Ctrl Pts',(0.717539045445532,-9.87174238998988,
2.14700383537712));
#94076=CARTESIAN_POINT('Ctrl Pts',(5.23689093707443,-8.39887691376832,2.22419044475824));
#94077=CARTESIAN_POINT('Ctrl Pts',(8.54846194734082,-4.98898370720772,2.30137705413935));
#94078=CARTESIAN_POINT('Ctrl Pts',(9.88850652481755,-0.428484309695933,
2.37856366352047));
#94079=CARTESIAN_POINT('Ctrl Pts',(8.94797102764415,4.23083615853781,2.45575027290158));
#94080=CARTESIAN_POINT('Ctrl Pts',(5.94377056743419,7.91440152493896,2.5329368822827));
#94081=CARTESIAN_POINT('Ctrl Pts',(1.56876202109868,9.77267342675648,2.61012349166382));
#94082=CARTESIAN_POINT('Ctrl Pts',(-3.16804913384846,9.37707975001673,2.68731010104494));
#94083=CARTESIAN_POINT('Ctrl Pts',(-7.17421508888992,6.81885607126705,2.76449671042605));
#94084=CARTESIAN_POINT('Ctrl Pts',(-9.52579632380792,2.68800381024176,2.84168331980716));
#94085=CARTESIAN_POINT('Ctrl Pts',(-9.6804490729513,-2.06278094755036,2.91886992918827));
#94086=CARTESIAN_POINT('Ctrl Pts',(-7.60250598055586,-6.33782810388617,
2.99605653856938));
#94087=CARTESIAN_POINT('Ctrl Pts',(-3.77120154294156,-9.15118537831773,
3.0732431479505));
#94088=CARTESIAN_POINT('Ctrl Pts',(0.929852459865417,-9.85401157969884,
3.15042975733161));
#94089=CARTESIAN_POINT('Ctrl Pts',(5.41645574070821,-8.28421110434545,3.22761636671273));
#94090=CARTESIAN_POINT('Ctrl Pts',(8.65386409648666,-4.80383245068529,3.30480297609384));
#94091=CARTESIAN_POINT('Ctrl Pts',(9.89543941191297,-0.215540528422498,
3.38198958547497));
#94092=CARTESIAN_POINT('Ctrl Pts',(8.85483132932753,4.422444779003,3.45917619485608));
#94093=CARTESIAN_POINT('Ctrl Pts',(5.77204772247514,8.04051720636283,3.53636280423719));
#94094=CARTESIAN_POINT('Ctrl Pts',(1.3580431887339,9.80414536331033,3.61354941361831));
#94095=CARTESIAN_POINT('Ctrl Pts',(-3.3691320474708,9.30677773243504,3.69073602299942));
#94096=CARTESIAN_POINT('Ctrl Pts',(-7.31935370725628,6.66274029288581,3.76792263238054));
#94097=CARTESIAN_POINT('Ctrl Pts',(-9.58138280765788,2.48258316453586,3.84510924176164));
#94098=CARTESIAN_POINT('Ctrl Pts',(-9.63395287216528,-2.27149912842799,
3.92230134240716));
#94099=CARTESIAN_POINT('Ctrl Pts',(-8.18687203103637,-5.09006448150602,
3.97376457325895));
#94100=CARTESIAN_POINT('Ctrl Pts',(-7.1762169795051,-6.2504122932827,3.99949893431705));
#94101=CARTESIAN_POINT('Ctrl Pts',(-7.17753992463813,-6.25025814508694,
4.));
#94102=CARTESIAN_POINT('Ctrl Pts',(-7.33747899506258,-6.07698634554822,
4.));
#94103=CARTESIAN_POINT('Ctrl Pts',(-7.49056477224393,-5.89798477017908,
4.));
#94104=CARTESIAN_POINT('Ctrl Pts',(-7.63665808758676,-5.71375997989628,
4.));
#94105=CARTESIAN_POINT('Ctrl Pts',(-7.78906164494726,-5.5215779260685,3.99999999999999));
#94106=CARTESIAN_POINT('Ctrl Pts',(-7.93385621938739,-5.32371142534202,
4.));
#94107=CARTESIAN_POINT('Ctrl Pts',(-8.07084803407231,-5.12068881632814,
4.));
#94108=CARTESIAN_POINT('Ctrl Pts',(-8.20560462808296,-4.920978816422,4.));
#94109=CARTESIAN_POINT('Ctrl Pts',(-8.33281124379099,-4.71627890600225,
4.));
#94110=CARTESIAN_POINT('Ctrl Pts',(-8.45224397122025,-4.50705565782589,
4.));
#94111=CARTESIAN_POINT('Ctrl Pts',(-8.57464826197255,-4.29262680023249,
4.));
#94112=CARTESIAN_POINT('Ctrl Pts',(-8.68888758368522,-4.07344621776482,
4.));
#94113=CARTESIAN_POINT('Ctrl Pts',(-8.7946726372693,-3.84998637008127,4.));
#94114=CARTESIAN_POINT('Ctrl Pts',(-8.90045769085338,-3.62652652239772,
4.));
#94115=CARTESIAN_POINT('Ctrl Pts',(-8.99778888243601,-3.39878676423124,
4.));
#94116=CARTESIAN_POINT('Ctrl Pts',(-9.08632214621229,-3.16721896610309,
3.99999999999999));
#94117=CARTESIAN_POINT('Ctrl Pts',(-9.09637755523444,-3.14091801629939,
3.99999999999999));
#94118=CARTESIAN_POINT('Ctrl Pts',(-9.10632000329729,-3.1145660732672,4.));
#94119=CARTESIAN_POINT('Ctrl Pts',(-9.11614707610044,-3.08816879512771,
4.));
#94120=CARTESIAN_POINT('Ctrl Pts',(-9.2011017289242,-2.8599653774107,4.));
#94121=CARTESIAN_POINT('Ctrl Pts',(-9.27721888532258,-2.6289661896699,3.99999999999999));
#94122=CARTESIAN_POINT('Ctrl Pts',(-9.34430660102968,-2.39565692690494,
3.99999999999999));
#94123=CARTESIAN_POINT('Ctrl Pts',(-9.36164354845565,-2.33536466057994,
3.99999999999999));
#94124=CARTESIAN_POINT('Ctrl Pts',(-9.37837727232265,-2.27491796400755,
3.99999999999999));
#94125=CARTESIAN_POINT('Ctrl Pts',(-9.39450398955669,-2.21432490746539,
3.99999999999999));
#94126=CARTESIAN_POINT('Ctrl Pts',(-9.45637742813918,-1.98184729233293,
3.99999999999999));
#94127=CARTESIAN_POINT('Ctrl Pts',(-9.50931939125301,-1.74721683731709,
4.));
#94128=CARTESIAN_POINT('Ctrl Pts',(-9.5534046592155,-1.51095720471577,3.99999999999999));
#94129=CARTESIAN_POINT('Ctrl Pts',(-9.59786987686295,-1.2726613641674,3.99999999999999));
#94130=CARTESIAN_POINT('Ctrl Pts',(-9.63332517643522,-1.03270751657381,
3.99999999999999));
#94131=CARTESIAN_POINT('Ctrl Pts',(-9.6597965096359,-0.791617070439592,
4.));
#94132=CARTESIAN_POINT('Ctrl Pts',(-9.68630729112195,-0.550167344904968,
4.));
#94133=CARTESIAN_POINT('Ctrl Pts',(-9.70380736090579,-0.307576969625407,
3.99999999999999));
#94134=CARTESIAN_POINT('Ctrl Pts',(-9.71227104245719,-0.0643635234899073,
3.99999999999999));
#94135=CARTESIAN_POINT('Ctrl Pts',(-9.71962412171651,0.14693551174726,4.));
#94136=CARTESIAN_POINT('Ctrl Pts',(-9.72015594631123,0.358705188501749,
4.));
#94137=CARTESIAN_POINT('Ctrl Pts',(-9.71381756308937,0.570603998902445,
4.));
#94138=CARTESIAN_POINT('Ctrl Pts',(-9.71288073663889,0.601923091399803,
4.));
#94139=CARTESIAN_POINT('Ctrl Pts',(-9.71179372592443,0.633244541288576,
4.));
#94140=CARTESIAN_POINT('Ctrl Pts',(-9.71055727203426,0.664548046919412,
4.));
#94141=CARTESIAN_POINT('Ctrl Pts',(-9.70089181440524,0.909250020620887,
4.));
#94142=CARTESIAN_POINT('Ctrl Pts',(-9.68209046391963,1.15315389789666,4.));
#94143=CARTESIAN_POINT('Ctrl Pts',(-9.6542249499493,1.3957320236345,4.));
#94144=CARTESIAN_POINT('Ctrl Pts',(-9.62623041699829,1.63943330046702,4.));
#94145=CARTESIAN_POINT('Ctrl Pts',(-9.58908764235844,1.88179718600469,4.));
#94146=CARTESIAN_POINT('Ctrl Pts',(-9.54281751783194,2.1222959970689,4.));
#94147=CARTESIAN_POINT('Ctrl Pts',(-9.52144752059438,2.23337110180816,4.));
#94148=CARTESIAN_POINT('Ctrl Pts',(-9.49812985694202,2.3440484113249,4.));
#94149=CARTESIAN_POINT('Ctrl Pts',(-9.47286282919077,2.45427585926503,4.));
#94150=CARTESIAN_POINT('Ctrl Pts',(-9.4182963957366,2.69232201024344,4.));
#94151=CARTESIAN_POINT('Ctrl Pts',(-9.35464183349599,2.92827092193509,4.00000000000001));
#94152=CARTESIAN_POINT('Ctrl Pts',(-9.28216423542203,3.16167818670979,4.00000000000001));
#94153=CARTESIAN_POINT('Ctrl Pts',(-9.20955177323737,3.39551976862565,4.00000000000001));
#94154=CARTESIAN_POINT('Ctrl Pts',(-9.12808315699099,3.62681083804243,4.));
#94155=CARTESIAN_POINT('Ctrl Pts',(-9.03797543804018,3.8550878224443,4.00000000000001));
#94156=CARTESIAN_POINT('Ctrl Pts',(-8.9872605556436,3.98356783006835,4.00000000000001));
#94157=CARTESIAN_POINT('Ctrl Pts',(-8.93380817564648,4.11109270907783,4.00000000000001));
#94158=CARTESIAN_POINT('Ctrl Pts',(-8.87765057142394,4.23757638926947,4.));
#94159=CARTESIAN_POINT('Ctrl Pts',(-8.86122721555927,4.27456668683681,4.00000000000001));
#94160=CARTESIAN_POINT('Ctrl Pts',(-8.84457048332952,4.31147200181025,4.00000000000001));
#94161=CARTESIAN_POINT('Ctrl Pts',(-8.82769641176815,4.34825743645122,4.00000000000001));
#94162=CARTESIAN_POINT('Ctrl Pts',(-8.72485965105928,4.5724413227164,4.00000000000001));
#94163=CARTESIAN_POINT('Ctrl Pts',(-8.61384851499838,4.79241839623982,4.00000000000001));
#94164=CARTESIAN_POINT('Ctrl Pts',(-8.49498741868439,5.00775935556626,4.00000000000001));
#94165=CARTESIAN_POINT('Ctrl Pts',(-8.37548461346274,5.22426290060047,4.00000000000001));
#94166=CARTESIAN_POINT('Ctrl Pts',(-8.24804660570247,5.43608074067127,4.00000000000001));
#94167=CARTESIAN_POINT('Ctrl Pts',(-8.11295177885207,5.64276338936583,4.00000000000001));
#94168=CARTESIAN_POINT('Ctrl Pts',(-7.97823605130347,5.84886605102726,4.00000000000001));
#94169=CARTESIAN_POINT('Ctrl Pts',(-7.83590610828956,6.04986288481014,4.00000000000001));
#94170=CARTESIAN_POINT('Ctrl Pts',(-7.68619142052777,6.2452862224332,4.00000000000001));
#94171=CARTESIAN_POINT('Ctrl Pts',(-7.57338204776326,6.39253686611006,4.));
#94172=CARTESIAN_POINT('Ctrl Pts',(-7.45637896623167,6.53662273702222,4.00000000000001));
#94173=CARTESIAN_POINT('Ctrl Pts',(-7.33526436842416,6.67733244061277,4.00000000000001));
#94174=CARTESIAN_POINT('Ctrl Pts',(-7.20393059754577,6.82991467517624,4.00000000000001));
#94175=CARTESIAN_POINT('Ctrl Pts',(-7.06776223834323,6.97852728621961,4.));
#94176=CARTESIAN_POINT('Ctrl Pts',(-6.92698192470154,7.12300597353219,4.));
#94177=CARTESIAN_POINT('Ctrl Pts',(-6.86539053748327,7.18621539923147,4.));
#94178=CARTESIAN_POINT('Ctrl Pts',(-6.80291619401115,7.24863334469569,4.));
#94179=CARTESIAN_POINT('Ctrl Pts',(-6.73957666848095,7.3102449686502,4.));
#94180=CARTESIAN_POINT('Ctrl Pts',(-6.71407204307116,7.33505382815293,4.));
#94181=CARTESIAN_POINT('Ctrl Pts',(-6.68842713210028,7.35973194343344,4.));
#94182=CARTESIAN_POINT('Ctrl Pts',(-6.66264307422955,7.38427831335995,4.));
#94183=CARTESIAN_POINT('Ctrl Pts',(-6.64018120243431,7.4056619689929,4.));
#94184=CARTESIAN_POINT('Ctrl Pts',(-6.61761358279404,7.42694571653633,4.));
#94185=CARTESIAN_POINT('Ctrl Pts',(-6.59495225244961,7.44811852242564,4.));
#94186=CARTESIAN_POINT('Ctrl Pts',(-6.41390307437516,7.61727536562624,3.99999999999999));
#94187=CARTESIAN_POINT('Ctrl Pts',(-6.22670562493156,7.77951670257842,4.));
#94188=CARTESIAN_POINT('Ctrl Pts',(-6.03383371121318,7.93459550516718,4.));
#94189=CARTESIAN_POINT('Ctrl Pts',(-5.8369373182061,8.09291019325686,4.));
#94190=CARTESIAN_POINT('Ctrl Pts',(-5.63412700431251,8.24376063630574,4.));
#94191=CARTESIAN_POINT('Ctrl Pts',(-5.42586722089454,8.38684532869713,4.));
#94192=CARTESIAN_POINT('Ctrl Pts',(-5.26967238333106,8.49415884799068,3.99999999999999));
#94193=CARTESIAN_POINT('Ctrl Pts',(-5.11041132947551,8.5971033880251,4.));
#94194=CARTESIAN_POINT('Ctrl Pts',(-4.94826783799957,8.69553540262911,4.));
#94195=CARTESIAN_POINT('Ctrl Pts',(-4.8988306475216,8.72554710529329,4.));
#94196=CARTESIAN_POINT('Ctrl Pts',(-4.84912543391596,8.75513920608326,3.99999999999999));
#94197=CARTESIAN_POINT('Ctrl Pts',(-4.79915724674574,8.78430735141901,3.99999999999999));
#94198=CARTESIAN_POINT('Ctrl Pts',(-4.75991954981983,8.80721174141972,3.99999999999999));
#94199=CARTESIAN_POINT('Ctrl Pts',(-4.72052093121596,8.8298538680067,3.99999999999999));
#94200=CARTESIAN_POINT('Ctrl Pts',(-4.68098377349437,8.85222069110153,3.99999999999999));
#94201=CARTESIAN_POINT('Ctrl Pts',(-4.46299777204146,8.97553897224803,3.99999999999999));
#94202=CARTESIAN_POINT('Ctrl Pts',(-4.24064631017737,9.09058408654495,3.99999999999999));
#94203=CARTESIAN_POINT('Ctrl Pts',(-4.01438141143131,9.19707375614046,3.99999999999999));
#94204=CARTESIAN_POINT('Ctrl Pts',(-3.81972428610794,9.28868749329092,3.99999999999999));
#94205=CARTESIAN_POINT('Ctrl Pts',(-3.62216994392975,9.3739686510575,3.99999999999999));
#94206=CARTESIAN_POINT('Ctrl Pts',(-3.42198933978191,9.45271162518228,3.99999999999999));
#94207=CARTESIAN_POINT('Ctrl Pts',(-3.18987047803637,9.54401782141498,3.99999999999999));
#94208=CARTESIAN_POINT('Ctrl Pts',(-2.95422044287104,9.62653433945234,3.99999999999999));
#94209=CARTESIAN_POINT('Ctrl Pts',(-2.715556454544,9.7002114681284,3.99999999999999));
#94210=CARTESIAN_POINT('Ctrl Pts',(-2.67798216851998,9.71181089511238,3.99999999999999));
#94211=CARTESIAN_POINT('Ctrl Pts',(-2.64033314728563,9.72319112812026,3.99999999999999));
#94212=CARTESIAN_POINT('Ctrl Pts',(-2.60261137764844,9.73435186015536,4.));
#94213=CARTESIAN_POINT('',(-7.17774563074874,-6.25019011963611,-8.27625731986589E-5));
#94214=CARTESIAN_POINT('Ctrl Pts',(-7.17208764054957,-6.25651381571847,
0.));
#94215=CARTESIAN_POINT('Ctrl Pts',(-7.17394681951216,-6.25438256581607,
-2.7587524399553E-5));
#94216=CARTESIAN_POINT('Ctrl Pts',(-7.17580504849477,-6.25225048720616,
-5.51750487991059E-5));
#94217=CARTESIAN_POINT('Ctrl Pts',(-7.177662326759,-6.25011758073595,-8.27625731986589E-5));
#94218=CARTESIAN_POINT('Ctrl Pts',(-2.60234962446759,9.73414364143212,-1.0842021724855E-19));
#94219=CARTESIAN_POINT('Ctrl Pts',(-2.83921919055991,9.66382362790923,1.12529727208794E-15));
#94220=CARTESIAN_POINT('Ctrl Pts',(-3.07300811801843,9.58476494231999,1.21052675641511E-15));
#94221=CARTESIAN_POINT('Ctrl Pts',(-3.30331680122151,9.49731112534334,1.74339709335669E-15));
#94222=CARTESIAN_POINT('Ctrl Pts',(-3.53610216223959,9.40891685347229,1.54456933875653E-15));
#94223=CARTESIAN_POINT('Ctrl Pts',(-3.76533259408592,9.31194565425811,1.1980971909858E-15));
#94224=CARTESIAN_POINT('Ctrl Pts',(-3.99058148198477,9.20670059788145,9.54097911787244E-16));
#94225=CARTESIAN_POINT('Ctrl Pts',(-4.21670322288308,9.10104771057611,5.48408101539471E-16));
#94226=CARTESIAN_POINT('Ctrl Pts',(-4.43881307462945,8.98705639487405,2.2267367935286E-15));
#94227=CARTESIAN_POINT('Ctrl Pts',(-4.65645683809879,8.86498601204875,2.69922972861991E-15));
#94228=CARTESIAN_POINT('Ctrl Pts',(-4.87235333431775,8.74389562322261,3.71048904750986E-15));
#94229=CARTESIAN_POINT('Ctrl Pts',(-5.08385566981937,8.61485497615695,2.80017349659852E-15));
#94230=CARTESIAN_POINT('Ctrl Pts',(-5.29049031594336,8.47807629762164,3.2612801348364E-15));
#94231=CARTESIAN_POINT('Ctrl Pts',(-5.42081859913753,8.39180746185063,3.14924689181288E-15));
#94232=CARTESIAN_POINT('Ctrl Pts',(-5.54920986020766,8.30245959621931,1.78699762241744E-15));
#94233=CARTESIAN_POINT('Ctrl Pts',(-5.67553765180558,8.21007850173578,1.83880688453542E-15));
#94234=CARTESIAN_POINT('Ctrl Pts',(-5.77028349550405,8.1407926808731,2.64557878001586E-15));
#94235=CARTESIAN_POINT('Ctrl Pts',(-5.8638685187314,8.06980054949169,2.65661309570741E-15));
#94236=CARTESIAN_POINT('Ctrl Pts',(-5.9562368606778,7.9971194985086,2.49106291150269E-15));
#94237=CARTESIAN_POINT('Ctrl Pts',(-5.98417863604779,7.97513320366526,1.4537999406096E-15));
#94238=CARTESIAN_POINT('Ctrl Pts',(-6.0120107941499,7.95299094799323,1.58948515428829E-15));
#94239=CARTESIAN_POINT('Ctrl Pts',(-6.03972595387582,7.93069785471182,-1.17961196366423E-16));
#94240=CARTESIAN_POINT('Ctrl Pts',(-6.06885454317143,7.90726784872431,-1.91248462629996E-15));
#94241=CARTESIAN_POINT('Ctrl Pts',(-6.09784513215552,7.88367828862461,-6.97452302353175E-16));
#94242=CARTESIAN_POINT('Ctrl Pts',(-6.12669201119307,7.85993367550021,-6.80011602582908E-16));
#94243=CARTESIAN_POINT('Ctrl Pts',(-6.31817074079434,7.70232257483264,-5.64244381074444E-16));
#94244=CARTESIAN_POINT('Ctrl Pts',(-6.50339066876894,7.53782638481512,2.86787635648006E-15));
#94245=CARTESIAN_POINT('Ctrl Pts',(-6.68192791724629,7.36671835802232,1.77635683940025E-15));
#94246=CARTESIAN_POINT('Ctrl Pts',(-6.70470366833599,7.34489034251901,1.63711319672862E-15));
#94247=CARTESIAN_POINT('Ctrl Pts',(-6.72737062736575,7.32295467056579,1.21696534810119E-15));
#94248=CARTESIAN_POINT('Ctrl Pts',(-6.7499278780749,7.30091186031464,1.40165656858926E-15));
#94249=CARTESIAN_POINT('Ctrl Pts',(-6.92625813246103,7.12860299213362,2.35832437895416E-15));
#94250=CARTESIAN_POINT('Ctrl Pts',(-7.09588765341928,6.94975046126885,2.35575650814671E-15));
#94251=CARTESIAN_POINT('Ctrl Pts',(-7.25857969872179,6.76482962390105,1.85962356624714E-15));
#94252=CARTESIAN_POINT('Ctrl Pts',(-7.42201108691358,6.57906842641648,1.77113455101788E-15));
#94253=CARTESIAN_POINT('Ctrl Pts',(-7.5784421663849,6.38718308731999,7.63037625231977E-16));
#94254=CARTESIAN_POINT('Ctrl Pts',(-7.72759204547317,6.18962237682373,-3.46944695195361E-16));
#94255=CARTESIAN_POINT('Ctrl Pts',(-7.87627943705517,5.99267426729565,-1.38191786245987E-15));
#94256=CARTESIAN_POINT('Ctrl Pts',(-8.0177310300406,5.79008534630041,1.33121440589865E-15));
#94257=CARTESIAN_POINT('Ctrl Pts',(-8.15162295721404,5.58227599425002,-5.41233724504764E-16));
#94258=CARTESIAN_POINT('Ctrl Pts',(-8.26759776180428,5.4022752316585,-1.92647886301059E-15));
#94259=CARTESIAN_POINT('Ctrl Pts',(-8.37790018862867,5.21835713365747,-1.85568084733084E-15));
#94260=CARTESIAN_POINT('Ctrl Pts',(-8.48228916729079,5.03078516303735,-2.66453525910038E-15));
#94261=CARTESIAN_POINT('Ctrl Pts',(-8.5011201218663,4.99694864788359,-2.58432894335183E-15));
#94262=CARTESIAN_POINT('Ctrl Pts',(-8.51975862523132,4.96299286801841,-1.66636520228865E-15));
#94263=CARTESIAN_POINT('Ctrl Pts',(-8.53818920411381,4.92894583550654,-1.99840144432528E-15));
#94264=CARTESIAN_POINT('Ctrl Pts',(-8.6553554767611,4.71250315513553,-4.10921137120173E-15));
#94265=CARTESIAN_POINT('Ctrl Pts',(-8.76426888616404,4.49211411010674,-1.84066867355076E-16));
#94266=CARTESIAN_POINT('Ctrl Pts',(-8.86469562417359,4.26823837544914,-2.72004641033163E-15));
#94267=CARTESIAN_POINT('Ctrl Pts',(-8.96498221895465,4.04467505428677,-5.25248705154183E-15));
#94268=CARTESIAN_POINT('Ctrl Pts',(-9.05680611487477,3.81763418427641,-6.54395179005909E-15));
#94269=CARTESIAN_POINT('Ctrl Pts',(-9.13988927972611,3.5875484410629,-6.49480469405717E-15));
#94270=CARTESIAN_POINT('Ctrl Pts',(-9.17816975363287,3.48153669602212,-6.47216022535571E-15));
#94271=CARTESIAN_POINT('Ctrl Pts',(-9.21459400355786,3.37487826045069,-7.00076967452139E-15));
#94272=CARTESIAN_POINT('Ctrl Pts',(-9.24913132420256,3.26761417878569,-6.68909372336657E-15));
#94273=CARTESIAN_POINT('Ctrl Pts',(-9.32430828445378,3.03413377401809,-6.05927787474007E-15));
#94274=CARTESIAN_POINT('Ctrl Pts',(-9.39054843147571,2.79778427755245,-6.09227021689154E-15));
#94275=CARTESIAN_POINT('Ctrl Pts',(-9.44781377586706,2.55908919896884,-6.49480469405717E-15));
#94276=CARTESIAN_POINT('Ctrl Pts',(-9.50492485430018,2.32103713625129,-7.09737120362222E-15));
#94277=CARTESIAN_POINT('Ctrl Pts',(-9.55310943460919,2.08065144744669,-6.42576610657209E-15));
#94278=CARTESIAN_POINT('Ctrl Pts',(-9.5922782570777,1.83844915244229,-6.74460487459783E-15));
#94279=CARTESIAN_POINT('Ctrl Pts',(-9.61396155849863,1.70436941666152,-5.65810346699789E-15));
#94280=CARTESIAN_POINT('Ctrl Pts',(-9.63288100101979,1.56973298585168,-4.9195398534525E-15));
#94281=CARTESIAN_POINT('Ctrl Pts',(-9.64901457990071,1.43462840724832,-6.43929354282591E-15));
#94282=CARTESIAN_POINT('Ctrl Pts',(-9.65375213453723,1.39495554064496,-7.49285349155712E-15));
#94283=CARTESIAN_POINT('Ctrl Pts',(-9.65824979964318,1.35523807611954,-5.32935632051397E-15));
#94284=CARTESIAN_POINT('Ctrl Pts',(-9.66250344928149,1.31551343168508,-5.19029264012261E-15));
#94285=CARTESIAN_POINT('Ctrl Pts',(-9.68848629612735,1.07286078275713,-4.34084084773944E-15));
#94286=CARTESIAN_POINT('Ctrl Pts',(-9.70540243338582,0.829675528430131,
-3.52635615547212E-15));
#94287=CARTESIAN_POINT('Ctrl Pts',(-9.71327571138526,0.586476102990858,
-3.96904731303493E-15));
#94288=CARTESIAN_POINT('Ctrl Pts',(-9.72116115923157,0.342900760459978,
-4.41242274512731E-15));
#94289=CARTESIAN_POINT('Ctrl Pts',(-9.71997579260738,0.0993105370203054,
-4.56754410064086E-15));
#94290=CARTESIAN_POINT('Ctrl Pts',(-9.70969161124852,-0.143779945942933,
-3.63598040564739E-15));
#94291=CARTESIAN_POINT('Ctrl Pts',(-9.69949621789526,-0.384771718429206,
-2.71245932286486E-15));
#94292=CARTESIAN_POINT('Ctrl Pts',(-9.68035838589556,-0.625272978090111,
2.79940693609296E-15));
#94293=CARTESIAN_POINT('Ctrl Pts',(-9.65220018038254,-0.864778715928871,
3.77475828372553E-15));
#94294=CARTESIAN_POINT('Ctrl Pts',(-9.63108916824546,-1.04434301863547,
4.50600708891906E-15));
#94295=CARTESIAN_POINT('Ctrl Pts',(-9.60490683713541,-1.22334772921605,
2.71191758976982E-15));
#94296=CARTESIAN_POINT('Ctrl Pts',(-9.5736016261349,-1.40157546597075,5.27355936696949E-15));
#94297=CARTESIAN_POINT('Ctrl Pts',(-9.54008130266794,-1.59241434537346,
7.34930365900901E-15));
#94298=CARTESIAN_POINT('Ctrl Pts',(-9.50068749895529,-1.78236265639502,
9.6353898453109E-15));
#94299=CARTESIAN_POINT('Ctrl Pts',(-9.45550504145372,-1.97116932539336,
8.24340595784179E-15));
#94300=CARTESIAN_POINT('Ctrl Pts',(-9.43573771629679,-2.05377224308013,
7.6084078733068E-15));
#94301=CARTESIAN_POINT('Ctrl Pts',(-9.41486216561421,-2.13615652108099,
6.2416746576837E-15));
#94302=CARTESIAN_POINT('Ctrl Pts',(-9.39288439672517,-2.21830049798781,
5.68989300120393E-15));
#94303=CARTESIAN_POINT('Ctrl Pts',(-9.38127566596173,-2.2616892203174,5.67346700880721E-15));
#94304=CARTESIAN_POINT('Ctrl Pts',(-9.36935940676183,-2.30501089184594,
1.02851375672538E-14));
#94305=CARTESIAN_POINT('Ctrl Pts',(-9.35713643218052,-2.34826227004022,
8.90953977261688E-15));
#94306=CARTESIAN_POINT('Ctrl Pts',(-9.34817714544189,-2.37996498663392,
7.90124387891348E-15));
#94307=CARTESIAN_POINT('Ctrl Pts',(-9.33905531224074,-2.41162191029918,
8.29834598157197E-15));
#94308=CARTESIAN_POINT('Ctrl Pts',(-9.32977348840701,-2.44322524102662,
8.27116153345742E-15));
#94309=CARTESIAN_POINT('Ctrl Pts',(-9.3091309585129,-2.51351020990564,8.21070404224538E-15));
#94310=CARTESIAN_POINT('Ctrl Pts',(-9.28769421535577,-2.58354046496828,
8.78374978742755E-15));
#94311=CARTESIAN_POINT('Ctrl Pts',(-9.26547044027429,-2.65330324410549,
8.99280649946377E-15));
#94312=CARTESIAN_POINT('Ctrl Pts',(-9.19195459005424,-2.88407726891374,
9.68436236129214E-15));
#94313=CARTESIAN_POINT('Ctrl Pts',(-9.10983017570767,-3.11192569697261,
9.50023376670274E-15));
#94314=CARTESIAN_POINT('Ctrl Pts',(-9.01932453558736,-3.33637613353048,
9.82547376793264E-15));
#94315=CARTESIAN_POINT('Ctrl Pts',(-8.93690619259326,-3.54077039051611,
1.0121651353563E-14));
#94316=CARTESIAN_POINT('Ctrl Pts',(-8.84753678016074,-3.74234696279182,
9.54369029972911E-15));
#94317=CARTESIAN_POINT('Ctrl Pts',(-8.75135419307074,-3.94073284400927,
9.76996261670138E-15));
#94318=CARTESIAN_POINT('Ctrl Pts',(-8.67921725275325,-4.08952225492236,
9.93966685443058E-15));
#94319=CARTESIAN_POINT('Ctrl Pts',(-8.60324722754804,-4.23651661611678,
6.6596841948106E-15));
#94320=CARTESIAN_POINT('Ctrl Pts',(-8.52349134733745,-4.38155083638406,
6.77236045021345E-15));
#94321=CARTESIAN_POINT('Ctrl Pts',(-8.49892470414398,-4.42622470783708,
6.80706732518681E-15));
#94322=CARTESIAN_POINT('Ctrl Pts',(-8.47399672617423,-4.47071593837625,
1.1327567305792E-14));
#94323=CARTESIAN_POINT('Ctrl Pts',(-8.44872639902523,-4.51498916092465,
1.04360964314765E-14));
#94324=CARTESIAN_POINT('Ctrl Pts',(-8.32958798602576,-4.72371781891507,
6.23320564280544E-15));
#94325=CARTESIAN_POINT('Ctrl Pts',(-8.20276674746981,-4.92774606792883,
6.92432169967517E-15));
#94326=CARTESIAN_POINT('Ctrl Pts',(-8.06846284876383,-5.12660291388634,
6.55031584528842E-15));
#94327=CARTESIAN_POINT('Ctrl Pts',(-7.95380311179895,-5.29637366418355,
6.23101451970896E-15));
#94328=CARTESIAN_POINT('Ctrl Pts',(-7.83368869300271,-5.46237501931451,
5.51132532032376E-15));
#94329=CARTESIAN_POINT('Ctrl Pts',(-7.70821972408079,-5.62429632476034,
4.49640324973188E-15));
#94330=CARTESIAN_POINT('Ctrl Pts',(-7.5607553014238,-5.81460339453705,3.00534834520389E-15));
#94331=CARTESIAN_POINT('Ctrl Pts',(-7.40589476781386,-5.99927566766814,
4.03884969480374E-15));
#94332=CARTESIAN_POINT('Ctrl Pts',(-7.24403669908448,-6.17797143930764,
1.72084568816899E-15));
#94333=CARTESIAN_POINT('Ctrl Pts',(-7.22210430648793,-6.20218540559124,
1.40674720476935E-15));
#94334=CARTESIAN_POINT('Ctrl Pts',(-7.20004338176182,-6.22628957396681,
7.04844233411283E-16));
#94335=CARTESIAN_POINT('Ctrl Pts',(-7.17785487282089,-6.25028303501658,
1.77635683940025E-15));
#94336=CARTESIAN_POINT('Origin',(0.,0.,4.));
#94337=CARTESIAN_POINT('',(-14.,-1.71450551880629E-15,4.));
#94338=CARTESIAN_POINT('Origin',(0.,0.,4.));
#94339=CARTESIAN_POINT('Origin',(0.,0.,0.));
#94340=CARTESIAN_POINT('',(-14.,-1.71450551880629E-15,0.));
#94341=CARTESIAN_POINT('',(-14.,-1.71450551880629E-15,0.));
#94342=CARTESIAN_POINT('Origin',(0.,0.,0.));
#94343=CARTESIAN_POINT('Origin',(0.,0.,0.));
#94392=UNCERTAINTY_MEASURE_WITH_UNIT(LENGTH_MEASURE(0.01),#94413,
'DISTANCE_ACCURACY_VALUE',
'Maximum model space distance between geometric entities at asserted c
onnectivities');
#94394=UNCERTAINTY_MEASURE_WITH_UNIT(LENGTH_MEASURE(0.01),#94413,
'DISTANCE_ACCURACY_VALUE',
'Maximum model space distance between geometric entities at asserted c
onnectivities');
#94410=(
GEOMETRIC_REPRESENTATION_CONTEXT(3)
GLOBAL_UNCERTAINTY_ASSIGNED_CONTEXT((#94392))
GLOBAL_UNIT_ASSIGNED_CONTEXT((#94413,#94415,#94416))
REPRESENTATION_CONTEXT('','3D')
);
#94412=(
GEOMETRIC_REPRESENTATION_CONTEXT(3)
GLOBAL_UNCERTAINTY_ASSIGNED_CONTEXT((#94394))
GLOBAL_UNIT_ASSIGNED_CONTEXT((#94413,#94415,#94416))
REPRESENTATION_CONTEXT('','3D')
);
#94413=(
LENGTH_UNIT()
NAMED_UNIT(*)
SI_UNIT(.MILLI.,.METRE.)
);
#94415=(
NAMED_UNIT(*)
PLANE_ANGLE_UNIT()
SI_UNIT($,.RADIAN.)
);
#94416=(
NAMED_UNIT(*)
SI_UNIT($,.STERADIAN.)
SOLID_ANGLE_UNIT()
);
#94432=SHAPE_DEFINITION_REPRESENTATION(#94466,#94501);
#94466=PRODUCT_DEFINITION_SHAPE('',$,#94519);
#94501=SHAPE_REPRESENTATION('',(#8889),#94410);
#94503=PRODUCT_DEFINITION_CONTEXT('part definition',#94556,'design');
#94519=PRODUCT_DEFINITION('Entry locknut','Entry locknut',#94536,#94503);
#94536=PRODUCT_DEFINITION_FORMATION('',$,#94573);
#94556=APPLICATION_CONTEXT(
'Core Data for Automotive Mechanical Design Process');
#94557=PRODUCT_CONTEXT('part definition',#94556,'mechanical');
#94573=PRODUCT('Entry locknut','Entry locknut',$,(#94557));
#94581=PRESENTATION_STYLE_ASSIGNMENT((#94588));
#94588=SURFACE_STYLE_USAGE(.BOTH.,#94595);
#94595=SURFACE_SIDE_STYLE('',(#94602));
#94602=SURFACE_STYLE_FILL_AREA(#94609);
#94609=FILL_AREA_STYLE('Opaque(185,192,202)',(#94616));
#94616=FILL_AREA_STYLE_COLOUR('Opaque(185,192,202)',#94623);
#94623=COLOUR_RGB('Opaque(185,192,202)',0.725490196078431,0.752941176470588,
0.792156862745098);
ENDSEC;
END-ISO-10303-21;
